ISO-10303-21;
HEADER;
FILE_DESCRIPTION (('STEP AP214'),
    '1' );
FILE_NAME ('Outer shift plate.step',
    '2026-10-12T23:53:07',
    ( '' ),
    ( '' ),
    'SwSTEP 2.0',
    'SolidWorks 2024',
    '' );
FILE_SCHEMA (( 'AUTOMOTIVE_DESIGN' ));
ENDSEC;

DATA;
#22=ADVANCED_FACE ( 'NONE', ( #25039 ), #12689, .F. ) ;
#40=ORIENTED_EDGE ( 'NONE', *, *, #699, .T. ) ;
#55=LINE ( 'NONE', #28391, #16768 ) ;
#83=PLANE ( 'NONE',  #29685 ) ;
#103=CARTESIAN_POINT ( 'NONE',  ( -0.08000000000000000167, -2.183180860297908144, -0.4937760292030871079 ) ) ;
#106=VECTOR ( 'NONE', #18794, 39.37007874015748143 ) ;
#111=CYLINDRICAL_SURFACE ( 'NONE', #1726, 0.7043128707267513056 ) ;
#121=ORIENTED_EDGE ( 'NONE', *, *, #38880, .F. ) ;
#135=ORIENTED_EDGE ( 'NONE', *, *, #17010, .F. ) ;
#175=DIRECTION ( 'NONE',  ( 0.000000000000000000, 0.7516797646744243222, -0.6595282642760672553 ) ) ;
#179=ORIENTED_EDGE ( 'NONE', *, *, #9391, .T. ) ;
#189=AXIS2_PLACEMENT_3D ( 'NONE', #3943, #19789, #32329 ) ;
#192=CARTESIAN_POINT ( 'NONE',  ( -0.02000000000000000042, -2.183180860297908144, -0.4937760292030871079 ) ) ;
#194=EDGE_CURVE ( 'NONE', #7245, #4305, #16385, .T. ) ;
#197=DIRECTION ( 'NONE',  ( 0.000000000000000000, 0.000000000000000000, 1.000000000000000000 ) ) ;
#209=ORIENTED_EDGE ( 'NONE', *, *, #39795, .T. ) ;
#212=ORIENTED_EDGE ( 'NONE', *, *, #27885, .F. ) ;
#216=EDGE_CURVE ( 'NONE', #890, #37816, #37994, .T. ) ;
#226=CARTESIAN_POINT ( 'NONE',  ( -0.02000000000000000042, -1.999693152383498207, -0.3073943322174670922 ) ) ;
#253=VECTOR ( 'NONE', #21136, 39.37007874015748143 ) ;
#255=AXIS2_PLACEMENT_3D ( 'NONE', #6297, #37978, #40241 ) ;
#265=ORIENTED_EDGE ( 'NONE', *, *, #7185, .T. ) ;
#274=EDGE_CURVE ( 'NONE', #16107, #30911, #31280, .T. ) ;
#283=CIRCLE ( 'NONE', #37664, 0.07999999999999996003 ) ;
#293=DIRECTION ( 'NONE',  ( 0.000000000000000000, 0.000000000000000000, -1.000000000000000000 ) ) ;
#301=ORIENTED_EDGE ( 'NONE', *, *, #27603, .T. ) ;
#302=ORIENTED_EDGE ( 'NONE', *, *, #13793, .F. ) ;
#311=AXIS2_PLACEMENT_3D ( 'NONE', #4661, #14149, #11266 ) ;
#339=DIRECTION ( 'NONE',  ( 0.000000000000000000, 0.000000000000000000, -1.000000000000000000 ) ) ;
#371=CIRCLE ( 'NONE', #14113, 0.08000000000000000167 ) ;
#376=AXIS2_PLACEMENT_3D ( 'NONE', #39921, #11130, #1488 ) ;
#387=EDGE_CURVE ( 'NONE', #5797, #36330, #29303, .T. ) ;
#397=AXIS2_PLACEMENT_3D ( 'NONE', #958, #6665, #10380 ) ;
#404=ADVANCED_FACE ( 'NONE', ( #14313 ), #17794, .F. ) ;
#407=DIRECTION ( 'NONE',  ( 0.000000000000000000, 0.000000000000000000, -1.000000000000000000 ) ) ;
#411=LINE ( 'NONE', #35317, #2910 ) ;
#412=CARTESIAN_POINT ( 'NONE',  ( -0.05464101615137763324, -1.772778095317936620, -0.3120197613628935551 ) ) ;
#416=VECTOR ( 'NONE', #18339, 39.37007874015748143 ) ;
#434=CARTESIAN_POINT ( 'NONE',  ( -0.02000000000000000042, -1.599201040860868339, 0.1642182323853691728 ) ) ;
#435=DIRECTION ( 'NONE',  ( 0.000000000000000000, 0.000000000000000000, -1.000000000000000000 ) ) ;
#439=DIRECTION ( 'NONE',  ( 0.000000000000000000, 0.000000000000000000, -1.000000000000000000 ) ) ;
#443=DIRECTION ( 'NONE',  ( 0.000000000000000000, -0.9215515678030121727, -0.3882559824134206306 ) ) ;
#494=DIRECTION ( 'NONE',  ( 0.000000000000000000, 0.000000000000000000, -1.000000000000000000 ) ) ;
#519=CARTESIAN_POINT ( 'NONE',  ( -0.05464101615137796630, -1.646519645934556131, -0.1171471737359304072 ) ) ;
#538=ADVANCED_FACE ( 'NONE', ( #23087 ), #29927, .T. ) ;
#557=DIRECTION ( 'NONE',  ( 0.000000000000000000, 0.6595282642760673664, 0.7516797646744242112 ) ) ;
#560=DIRECTION ( 'NONE',  ( 0.000000000000000000, 0.000000000000000000, -1.000000000000000000 ) ) ;
#562=ORIENTED_EDGE ( 'NONE', *, *, #194, .F. ) ;
#573=UNCERTAINTY_MEASURE_WITH_UNIT (LENGTH_MEASURE( 1.000000000000000082E-05 ), #35025, 'distance_accuracy_value', 'NONE');
#641=VERTEX_POINT ( 'NONE', #3184 ) ;
#655=EDGE_LOOP ( 'NONE', ( #20187, #33191, #212, #10371 ) ) ;
#657=LINE ( 'NONE', #28987, #16108 ) ;
#662=EDGE_CURVE ( 'NONE', #20865, #4083, #9046, .T. ) ;
#696=ORIENTED_EDGE ( 'NONE', *, *, #15763, .F. ) ;
#698=DIRECTION ( 'NONE',  ( 1.000000000000000000, 0.000000000000000000, 0.000000000000000000 ) ) ;
#699=EDGE_CURVE ( 'NONE', #12256, #34558, #5748, .T. ) ;
#719=ADVANCED_FACE ( 'NONE', ( #36020 ), #10368, .F. ) ;
#733=CARTESIAN_POINT ( 'NONE',  ( -0.02000000000000000042, -2.266124458208340187, -0.5531721439363799231 ) ) ;
#746=ORIENTED_EDGE ( 'NONE', *, *, #7185, .F. ) ;
#768=VECTOR ( 'NONE', #1242, 39.37007874015748143 ) ;
#769=EDGE_CURVE ( 'NONE', #31675, #29116, #15627, .T. ) ;
#782=DIRECTION ( 'NONE',  ( 1.000000000000000000, -0.000000000000000000, -0.000000000000000000 ) ) ;
#787=DIRECTION ( 'NONE',  ( 1.000000000000000000, 0.000000000000000000, 0.000000000000000000 ) ) ;
#793=CARTESIAN_POINT ( 'NONE',  ( -0.02000000000000000042, -2.177105168660885326, -0.3918349584362407212 ) ) ;
#827=VECTOR ( 'NONE', #40287, 39.37007874015748143 ) ;
#843=DIRECTION ( 'NONE',  ( 1.000000000000000000, 0.000000000000000000, 0.000000000000000000 ) ) ;
#867=AXIS2_PLACEMENT_3D ( 'NONE', #16303, #28430, #10117 ) ;
#883=AXIS2_PLACEMENT_3D ( 'NONE', #24131, #20412, #8048 ) ;
#890=VERTEX_POINT ( 'NONE', #1064 ) ;
#897=CARTESIAN_POINT ( 'NONE',  ( -0.05464101615137773038, -2.698373762442814350, -0.2370085142459261718 ) ) ;
#900=ORIENTED_EDGE ( 'NONE', *, *, #32662, .T. ) ;
#915=CARTESIAN_POINT ( 'NONE',  ( -0.02000000000000000042, -2.626773565144302935, -0.2526934094652523721 ) ) ;
#922=VECTOR ( 'NONE', #37613, 39.37007874015748143 ) ;
#947=DIRECTION ( 'NONE',  ( -1.000000000000000000, 0.000000000000000000, 0.000000000000000000 ) ) ;
#958=CARTESIAN_POINT ( 'NONE',  ( -0.02000000000000000042, -1.699711333021935777, -0.9366211149475224262 ) ) ;
#981=AXIS2_PLACEMENT_3D ( 'NONE', #34205, #18797, #21888 ) ;
#1013=CARTESIAN_POINT ( 'NONE',  ( -0.08000000000000000167, -2.183180860297908144, -0.3317586832283064280 ) ) ;
#1025=DIRECTION ( 'NONE',  ( 1.000000000000000000, -0.000000000000000000, -0.000000000000000000 ) ) ;
#1035=CIRCLE ( 'NONE', #2321, 0.08000000000000000167 ) ;
#1046=DIRECTION ( 'NONE',  ( 0.000000000000000000, 0.000000000000000000, 1.000000000000000000 ) ) ;
#1060=PLANE ( 'NONE',  #23186 ) ;
#1064=CARTESIAN_POINT ( 'NONE',  ( -0.05464101615137762630, -1.772778095317936620, -0.3120197613628934441 ) ) ;
#1065=CARTESIAN_POINT ( 'NONE',  ( -0.05464101615137785528, -2.314906514113384883, -0.5881050943081593818 ) ) ;
#1092=LINE ( 'NONE', #3739, #26311 ) ;
#1104=CARTESIAN_POINT ( 'NONE',  ( -0.05464101615137796630, -1.706654027108509997, -0.06438491259384498955 ) ) ;
#1122=FACE_OUTER_BOUND ( 'NONE', #19630, .T. ) ;
#1126=( CONVERSION_BASED_UNIT ( 'INCH', #10967 ) LENGTH_UNIT ( ) NAMED_UNIT ( #23398 ) );
#1152=VERTEX_POINT ( 'NONE', #1594 ) ;
#1200=EDGE_CURVE ( 'NONE', #15916, #5177, #13017, .T. ) ;
#1207=CARTESIAN_POINT ( 'NONE',  ( -0.08000000000000000167, -1.750394882718339762, -0.1142373872069606250 ) ) ;
#1226=EDGE_CURVE ( 'NONE', #23547, #31675, #11053, .T. ) ;
#1242=DIRECTION ( 'NONE',  ( 1.000000000000000000, -0.000000000000000000, -0.000000000000000000 ) ) ;
#1282=EDGE_LOOP ( 'NONE', ( #31892, #34657, #27826, #15822 ) ) ;
#1311=CARTESIAN_POINT ( 'NONE',  ( -0.02000000000000000042, -1.944084441611813707, -0.4562887203618206655 ) ) ;
#1312=DIRECTION ( 'NONE',  ( -1.000000000000000000, -0.000000000000000000, -0.000000000000000000 ) ) ;
#1315=DIRECTION ( 'NONE',  ( 0.000000000000000000, -0.5127411190260188212, -0.8585432690668224343 ) ) ;
#1324=ORIENTED_EDGE ( 'NONE', *, *, #38545, .T. ) ;
#1332=ORIENTED_EDGE ( 'NONE', *, *, #18204, .T. ) ;
#1334=VERTEX_POINT ( 'NONE', #37958 ) ;
#1351=CARTESIAN_POINT ( 'NONE',  ( -0.05464101615137761936, -1.845925619402022155, -0.2644148183989317724 ) ) ;
#1362=CARTESIAN_POINT ( 'NONE',  ( -0.05464101615137762630, -1.910390638264138685, -0.8220407338378623585 ) ) ;
#1376=DIRECTION ( 'NONE',  ( 0.000000000000000000, 0.000000000000000000, 1.000000000000000000 ) ) ;
#1384=CARTESIAN_POINT ( 'NONE',  ( -0.05464101615137773038, -2.585754275622221154, -0.2040099479399058724 ) ) ;
#1402=CIRCLE ( 'NONE', #24374, 0.1400000000000008182 ) ;
#1432=DIRECTION ( 'NONE',  ( 1.000000000000000000, 0.000000000000000000, 0.000000000000000000 ) ) ;
#1481=ORIENTED_EDGE ( 'NONE', *, *, #14908, .F. ) ;
#1485=ORIENTED_EDGE ( 'NONE', *, *, #25566, .T. ) ;
#1488=DIRECTION ( 'NONE',  ( 0.000000000000000000, 0.000000000000000000, 1.000000000000000000 ) ) ;
#1498=EDGE_CURVE ( 'NONE', #19084, #27272, #2137, .T. ) ;
#1523=DIRECTION ( 'NONE',  ( 0.000000000000000000, 0.000000000000000000, 1.000000000000000000 ) ) ;
#1541=CIRCLE ( 'NONE', #35666, 0.07999999999999996003 ) ;
#1562=CARTESIAN_POINT ( 'NONE',  ( -0.02000000000000000042, -1.910390638264138685, -0.7420407338378623985 ) ) ;
#1582=CARTESIAN_POINT ( 'NONE',  ( -0.08000000000000000167, -2.367354784411275670, -0.3586747285825516718 ) ) ;
#1594=CARTESIAN_POINT ( 'NONE',  ( -0.02000000000000000042, -2.402843508890908808, -0.4070539641574215106 ) ) ;
#1626=VECTOR ( 'NONE', #16951, 39.37007874015748854 ) ;
#1628=PLANE ( 'NONE',  #7464 ) ;
#1657=EDGE_CURVE ( 'NONE', #16708, #39344, #7950, .T. ) ;
#1662=EDGE_CURVE ( 'NONE', #12973, #30547, #29671, .T. ) ;
#1720=CARTESIAN_POINT ( 'NONE',  ( -0.02000000000000000042, -1.845925619402022155, -0.3444148183989317880 ) ) ;
#1726=AXIS2_PLACEMENT_3D ( 'NONE', #29057, #3157, #25789 ) ;
#1767=ORIENTED_EDGE ( 'NONE', *, *, #6638, .T. ) ;
#1783=DIRECTION ( 'NONE',  ( 1.000000000000000000, 0.000000000000000000, 0.000000000000000000 ) ) ;
#1795=DIRECTION ( 'NONE',  ( 0.000000000000000000, 0.000000000000000000, 1.000000000000000000 ) ) ;
#1840=VERTEX_POINT ( 'NONE', #1013 ) ;
#1863=LINE ( 'NONE', #17486, #5565 ) ;
#1873=DIRECTION ( 'NONE',  ( 0.000000000000000000, 0.000000000000000000, -1.000000000000000000 ) ) ;
#1879=CARTESIAN_POINT ( 'NONE',  ( -0.08000000000000000167, -1.682484669133182953, -0.03683853088544705029 ) ) ;
#1882=EDGE_CURVE ( 'NONE', #13458, #18110, #25067, .T. ) ;
#1886=EDGE_CURVE ( 'NONE', #38792, #40536, #8353, .T. ) ;
#1921=ORIENTED_EDGE ( 'NONE', *, *, #21052, .T. ) ;
#1987=DIRECTION ( 'NONE',  ( 1.000000000000000000, -0.000000000000000000, -0.000000000000000000 ) ) ;
#2005=LINE ( 'NONE', #29983, #10863 ) ;
#2018=EDGE_CURVE ( 'NONE', #5177, #14867, #34667, .T. ) ;
#2043=EDGE_CURVE ( 'NONE', #2067, #2801, #34860, .T. ) ;
#2044=LINE ( 'NONE', #39277, #16115 ) ;
#2055=VECTOR ( 'NONE', #31921, 39.37007874015748143 ) ;
#2067=VERTEX_POINT ( 'NONE', #18849 ) ;
#2068=VERTEX_POINT ( 'NONE', #6669 ) ;
#2083=CIRCLE ( 'NONE', #25048, 0.1620173459747806799 ) ;
#2137=LINE ( 'NONE', #13852, #9903 ) ;
#2146=DIRECTION ( 'NONE',  ( 1.000000000000000000, -0.000000000000000000, -0.000000000000000000 ) ) ;
#2148=VECTOR ( 'NONE', #18130, 39.37007874015748143 ) ;
#2173=ORIENTED_EDGE ( 'NONE', *, *, #1498, .T. ) ;
#2174=CARTESIAN_POINT ( 'NONE',  ( -0.02000000000000000042, -1.723343441215260619, -0.2604803408413784993 ) ) ;
#2176=CIRCLE ( 'NONE', #3493, 0.4488493849861021068 ) ;
#2208=ADVANCED_FACE ( 'NONE', ( #30251 ), #39318, .T. ) ;
#2210=AXIS2_PLACEMENT_3D ( 'NONE', #12468, #33663, #30793 ) ;
#2236=VERTEX_POINT ( 'NONE', #12554 ) ;
#2243=CIRCLE ( 'NONE', #35049, 0.5756329413417604624 ) ;
#2249=EDGE_LOOP ( 'NONE', ( #29412, #7120, #1767, #19083 ) ) ;
#2253=DIRECTION ( 'NONE',  ( 1.000000000000000000, 0.000000000000000000, 0.000000000000000000 ) ) ;
#2320=CONICAL_SURFACE ( 'NONE', #23332, 0.1400000000000013178, 1.047197551196602072 ) ;
#2321=AXIS2_PLACEMENT_3D ( 'NONE', #22952, #17161, #29105 ) ;
#2336=ORIENTED_EDGE ( 'NONE', *, *, #28866, .F. ) ;
#2361=AXIS2_PLACEMENT_3D ( 'NONE', #4215, #12883, #13077 ) ;
#2406=DIRECTION ( 'NONE',  ( 1.000000000000000000, 0.000000000000000000, 0.000000000000000000 ) ) ;
#2422=DIRECTION ( 'NONE',  ( 0.000000000000000000, 0.000000000000000000, -1.000000000000000000 ) ) ;
#2452=ADVANCED_FACE ( 'NONE', ( #23047 ), #7174, .T. ) ;
#2519=SHAPE_DEFINITION_REPRESENTATION ( #7127, #9349 ) ;
#2542=DIRECTION ( 'NONE',  ( -0.4999999999999955036, 0.7088756765536057269, 0.4974889699186023639 ) ) ;
#2552=CARTESIAN_POINT ( 'NONE',  ( -0.05464101615137770263, -2.542046649843399564, -0.2305290188067205537 ) ) ;
#2560=DIRECTION ( 'NONE',  ( 0.000000000000000000, 0.000000000000000000, 1.000000000000000000 ) ) ;
#2637=ORIENTED_EDGE ( 'NONE', *, *, #30387, .F. ) ;
#2673=EDGE_LOOP ( 'NONE', ( #19685, #31629, #23451, #6716 ) ) ;
#2684=CARTESIAN_POINT ( 'NONE',  ( -0.08000000000000000167, -2.626773565144302935, -0.2726934094652516127 ) ) ;
#2695=CIRCLE ( 'NONE', #4634, 0.1400000000000009570 ) ;
#2703=CARTESIAN_POINT ( 'NONE',  ( -0.02000000000000000042, -2.577535374323032702, -0.2789082543815905590 ) ) ;
#2717=ORIENTED_EDGE ( 'NONE', *, *, #15763, .T. ) ;
#2725=EDGE_CURVE ( 'NONE', #1334, #8744, #25950, .T. ) ;
#2738=DIRECTION ( 'NONE',  ( -0.000000000000000000, -0.3882559824134205750, 0.9215515678030121727 ) ) ;
#2746=DIRECTION ( 'NONE',  ( 0.000000000000000000, 0.000000000000000000, -1.000000000000000000 ) ) ;
#2747=DIRECTION ( 'NONE',  ( 0.000000000000000000, 0.000000000000000000, -1.000000000000000000 ) ) ;
#2767=CARTESIAN_POINT ( 'NONE',  ( -0.08000000000000000167, -2.198867511061768809, -0.9423512173156428640 ) ) ;
#2769=VERTEX_POINT ( 'NONE', #17812 ) ;
#2789=VECTOR ( 'NONE', #15660, 39.37007874015748143 ) ;
#2801=VERTEX_POINT ( 'NONE', #11846 ) ;
#2803=PLANE ( 'NONE',  #22550 ) ;
#2820=CARTESIAN_POINT ( 'NONE',  ( -0.08000000000000000167, -2.551729310907437043, -0.5086726180052709712 ) ) ;
#2850=VECTOR ( 'NONE', #9839, 39.37007874015748143 ) ;
#2851=VECTOR ( 'NONE', #17766, 39.37007874015748143 ) ;
#2854=AXIS2_PLACEMENT_3D ( 'NONE', #32552, #20631, #35850 ) ;
#2855=DIRECTION ( 'NONE',  ( -0.4999999999999986677, 0.8653188367530366687, 0.03497585968025478109 ) ) ;
#2878=DIRECTION ( 'NONE',  ( -1.000000000000000000, -0.000000000000000000, -0.000000000000000000 ) ) ;
#2898=EDGE_CURVE ( 'NONE', #10878, #39409, #26584, .T. ) ;
#2910=VECTOR ( 'NONE', #6313, 39.37007874015748854 ) ;
#2925=ORIENTED_EDGE ( 'NONE', *, *, #31326, .F. ) ;
#2958=EDGE_CURVE ( 'NONE', #5177, #5941, #35115, .T. ) ;
#2960=EDGE_CURVE ( 'NONE', #4299, #18164, #20026, .T. ) ;
#2961=DIRECTION ( 'NONE',  ( 0.000000000000000000, 0.000000000000000000, 1.000000000000000000 ) ) ;
#3008=LINE ( 'NONE', #6066, #16049 ) ;
#3038=CIRCLE ( 'NONE', #2361, 0.1400000000000007627 ) ;
#3046=DIRECTION ( 'NONE',  ( -0.8660254037844408170, -0.3758398823372094966, 0.3297641321380312407 ) ) ;
#3057=CARTESIAN_POINT ( 'NONE',  ( -0.05464101615137773038, -1.599201040860868339, 0.1642182323853691728 ) ) ;
#3070=AXIS2_PLACEMENT_3D ( 'NONE', #21685, #21079, #2560 ) ;
#3073=DIRECTION ( 'NONE',  ( 0.000000000000000000, 0.000000000000000000, -1.000000000000000000 ) ) ;
#3074=DIRECTION ( 'NONE',  ( 0.000000000000000000, 0.000000000000000000, -1.000000000000000000 ) ) ;
#3081=DIRECTION ( 'NONE',  ( 1.000000000000000000, -0.000000000000000000, -0.000000000000000000 ) ) ;
#3085=EDGE_LOOP ( 'NONE', ( #27978, #22045, #5285, #3311 ) ) ;
#3092=LINE ( 'NONE', #24902, #7275 ) ;
#3094=ORIENTED_EDGE ( 'NONE', *, *, #35938, .T. ) ;
#3118=LINE ( 'NONE', #22458, #2789 ) ;
#3120=EDGE_CURVE ( 'NONE', #7245, #8808, #1035, .T. ) ;
#3127=FACE_OUTER_BOUND ( 'NONE', #3085, .T. ) ;
#3131=DIRECTION ( 'NONE',  ( -1.000000000000000000, -0.000000000000000000, -0.000000000000000000 ) ) ;
#3135=EDGE_LOOP ( 'NONE', ( #28077, #39870, #10460, #13950 ) ) ;
#3157=DIRECTION ( 'NONE',  ( -1.000000000000000000, -0.000000000000000000, -0.000000000000000000 ) ) ;
#3164=EDGE_CURVE ( 'NONE', #14867, #30658, #12830, .T. ) ;
#3184=CARTESIAN_POINT ( 'NONE',  ( -0.08000000000000000167, -2.274798198814180772, -0.3601501197397404264 ) ) ;
#3200=DIRECTION ( 'NONE',  ( 0.000000000000000000, 0.000000000000000000, -1.000000000000000000 ) ) ;
#3230=EDGE_CURVE ( 'NONE', #9944, #12909, #371, .T. ) ;
#3253=CARTESIAN_POINT ( 'NONE',  ( -0.08000000000000000167, -2.116970787486931460, -0.3045972195783253067 ) ) ;
#3258=DIRECTION ( 'NONE',  ( 0.000000000000000000, 0.3882559824134205195, -0.9215515678030119506 ) ) ;
#3266=CARTESIAN_POINT ( 'NONE',  ( -0.08000000000000000167, -2.183180860297908144, -0.4937760292030871079 ) ) ;
#3276=CARTESIAN_POINT ( 'NONE',  ( -0.02000000000000000042, -1.944084441611813707, -0.4562887203618206655 ) ) ;
#3289=ORIENTED_EDGE ( 'NONE', *, *, #13186, .F. ) ;
#3299=DIRECTION ( 'NONE',  ( -0.4999999999999968359, 0.8555732718332328401, 0.1341431195573592750 ) ) ;
#3304=CARTESIAN_POINT ( 'NONE',  ( -0.08000000000000000167, -1.851224977018630868, -0.7958870385335592434 ) ) ;
#3310=DIRECTION ( 'NONE',  ( -1.000000000000000000, -0.000000000000000000, -0.000000000000000000 ) ) ;
#3311=ORIENTED_EDGE ( 'NONE', *, *, #25118, .F. ) ;
#3333=CARTESIAN_POINT ( 'NONE',  ( -0.02000000000000000042, -2.183180860297908144, -0.4937760292030871079 ) ) ;
#3359=ORIENTED_EDGE ( 'NONE', *, *, #7666, .T. ) ;
#3378=AXIS2_PLACEMENT_3D ( 'NONE', #3057, #25883, #16215 ) ;
#3391=ADVANCED_FACE ( 'NONE', ( #27036 ), #31859, .F. ) ;
#3427=DIRECTION ( 'NONE',  ( 0.000000000000000000, 0.000000000000000000, -1.000000000000000000 ) ) ;
#3448=EDGE_CURVE ( 'NONE', #9944, #16485, #22106, .T. ) ;
#3493=AXIS2_PLACEMENT_3D ( 'NONE', #15473, #1783, #24184 ) ;
#3509=DIRECTION ( 'NONE',  ( 0.000000000000000000, -0.8063205929144885431, 0.5914787413272156735 ) ) ;
#3510=( GEOMETRIC_REPRESENTATION_CONTEXT ( 3 ) GLOBAL_UNCERTAINTY_ASSIGNED_CONTEXT ( ( #573 ) ) GLOBAL_UNIT_ASSIGNED_CONTEXT ( ( #35025, #6622, #18807 ) ) REPRESENTATION_CONTEXT ( 'NONE', 'WORKASPACE' ) );
#3569=AXIS2_PLACEMENT_3D ( 'NONE', #4848, #29558, #39016 ) ;
#3576=CARTESIAN_POINT ( 'NONE',  ( -0.02000000000000000042, -2.589364949149576933, -0.2950346662398796171 ) ) ;
#3611=CONICAL_SURFACE ( 'NONE', #26621, 0.1400000000000005684, 1.047197551196600518 ) ;
#3614=CARTESIAN_POINT ( 'NONE',  ( -0.02000000000000000042, -2.313818782766725146, -0.3979462133327477114 ) ) ;
#3660=ORIENTED_EDGE ( 'NONE', *, *, #10452, .T. ) ;
#3664=CARTESIAN_POINT ( 'NONE',  ( -0.08000000000000000167, -1.599201040860868339, 0.2442182323853691606 ) ) ;
#3680=CARTESIAN_POINT ( 'NONE',  ( -0.02000000000000000042, -2.058305985490972212, -0.5970033804171128722 ) ) ;
#3699=ORIENTED_EDGE ( 'NONE', *, *, #8675, .F. ) ;
#3706=FACE_OUTER_BOUND ( 'NONE', #16141, .T. ) ;
#3710=ORIENTED_EDGE ( 'NONE', *, *, #31086, .F. ) ;
#3735=EDGE_CURVE ( 'NONE', #5941, #27272, #27198, .T. ) ;
#3739=CARTESIAN_POINT ( 'NONE',  ( -0.08000000000000000167, -2.144840178508589545, -0.3363606153560244616 ) ) ;
#3745=VERTEX_POINT ( 'NONE', #3253 ) ;
#3789=DIRECTION ( 'NONE',  ( 0.000000000000000000, 0.000000000000000000, 1.000000000000000000 ) ) ;
#3874=LINE ( 'NONE', #12953, #38200 ) ;
#3890=CARTESIAN_POINT ( 'NONE',  ( -0.02000000000000000042, -1.910390638264138685, -0.7420407338378623985 ) ) ;
#3896=ORIENTED_EDGE ( 'NONE', *, *, #32123, .T. ) ;
#3910=CARTESIAN_POINT ( 'NONE',  ( -0.02000000000000000042, -1.699711333021935777, -0.9366211149475224262 ) ) ;
#3920=DIRECTION ( 'NONE',  ( -1.000000000000000000, -0.000000000000000000, -0.000000000000000000 ) ) ;
#3928=ORIENTED_EDGE ( 'NONE', *, *, #28813, .T. ) ;
#3943=CARTESIAN_POINT ( 'NONE',  ( -0.05464101615137787610, -2.551729310907437043, -0.5086726180052709712 ) ) ;
#3975=ORIENTED_EDGE ( 'NONE', *, *, #32047, .F. ) ;
#3996=EDGE_CURVE ( 'NONE', #890, #26070, #2005, .T. ) ;
#4006=VECTOR ( 'NONE', #16099, 39.37007874015748854 ) ;
#4017=CARTESIAN_POINT ( 'NONE',  ( -0.05464101615137770263, -2.320036485105098301, -0.3741690811493925128 ) ) ;
#4040=ORIENTED_EDGE ( 'NONE', *, *, #28813, .F. ) ;
#4075=DIRECTION ( 'NONE',  ( 1.000000000000000000, -0.000000000000000000, -0.000000000000000000 ) ) ;
#4083=VERTEX_POINT ( 'NONE', #32653 ) ;
#4091=CARTESIAN_POINT ( 'NONE',  ( -0.05464101615137785528, -2.253856486606507836, -0.7252438489935795207 ) ) ;
#4094=LINE ( 'NONE', #28402, #5586 ) ;
#4097=ADVANCED_FACE ( 'NONE', ( #38808 ), #8363, .T. ) ;
#4113=AXIS2_PLACEMENT_3D ( 'NONE', #10908, #6130, #34315 ) ;
#4118=AXIS2_PLACEMENT_3D ( 'NONE', #36614, #17674, #20582 ) ;
#4164=CIRCLE ( 'NONE', #21928, 0.01999999999999927530 ) ;
#4168=DIRECTION ( 'NONE',  ( 1.000000000000000000, 0.000000000000000000, 0.000000000000000000 ) ) ;
#4183=DIRECTION ( 'NONE',  ( 0.000000000000000000, 0.000000000000000000, 1.000000000000000000 ) ) ;
#4215=CARTESIAN_POINT ( 'NONE',  ( -0.02000000000000000042, -2.320036485105098301, -0.2941690811493925528 ) ) ;
#4226=DIRECTION ( 'NONE',  ( 0.000000000000000000, 0.3882559824134205195, -0.9215515678030121727 ) ) ;
#4280=CARTESIAN_POINT ( 'NONE',  ( -0.05464101615137763324, -2.183180860297908144, -0.4937760292030871079 ) ) ;
#4282=CARTESIAN_POINT ( 'NONE',  ( -0.05464101615137796630, -2.183180860297908144, -0.4937760292030871079 ) ) ;
#4284=CONICAL_SURFACE ( 'NONE', #37796, 0.1400000000000008182, 1.047197551196601850 ) ;
#4293=ORIENTED_EDGE ( 'NONE', *, *, #3230, .T. ) ;
#4299=VERTEX_POINT ( 'NONE', #11851 ) ;
#4305=VERTEX_POINT ( 'NONE', #25838 ) ;
#4306=AXIS2_PLACEMENT_3D ( 'NONE', #3614, #31585, #22161 ) ;
#4317=DIRECTION ( 'NONE',  ( 0.000000000000000000, 0.000000000000000000, -1.000000000000000000 ) ) ;
#4365=CYLINDRICAL_SURFACE ( 'NONE', #17334, 0.08000000000000000167 ) ;
#4395=CARTESIAN_POINT ( 'NONE',  ( -0.02000000000000000042, -2.320036485105098301, -0.2941690811493925528 ) ) ;
#4397=ORIENTED_EDGE ( 'NONE', *, *, #39795, .F. ) ;
#4410=ADVANCED_FACE ( 'NONE', ( #16564 ), #28902, .F. ) ;
#4479=EDGE_LOOP ( 'NONE', ( #10510, #34855, #301, #24747, #18777, #38044, #15171 ) ) ;
#4481=VERTEX_POINT ( 'NONE', #28505 ) ;
#4489=ORIENTED_EDGE ( 'NONE', *, *, #14426, .T. ) ;
#4520=ORIENTED_EDGE ( 'NONE', *, *, #12984, .T. ) ;
#4531=ORIENTED_EDGE ( 'NONE', *, *, #20282, .F. ) ;
#4597=AXIS2_PLACEMENT_3D ( 'NONE', #7516, #32812, #1376 ) ;
#4600=ORIENTED_EDGE ( 'NONE', *, *, #32849, .T. ) ;
#4634=AXIS2_PLACEMENT_3D ( 'NONE', #40616, #18615, #37944 ) ;
#4642=EDGE_CURVE ( 'NONE', #18399, #25808, #21425, .T. ) ;
#4656=CARTESIAN_POINT ( 'NONE',  ( -0.02000000000000000042, -2.698373762442814350, -0.2370085142459261163 ) ) ;
#4661=CARTESIAN_POINT ( 'NONE',  ( -0.02000000000000000042, -2.379949255320110257, -0.6346823614705312533 ) ) ;
#4665=ORIENTED_EDGE ( 'NONE', *, *, #6869, .F. ) ;
#4666=EDGE_CURVE ( 'NONE', #27138, #2769, #39143, .T. ) ;
#4671=VECTOR ( 'NONE', #21414, 39.37007874015748143 ) ;
#4736=AXIS2_PLACEMENT_3D ( 'NONE', #26213, #38736, #10560 ) ;
#4745=DIRECTION ( 'NONE',  ( 0.000000000000000000, 0.000000000000000000, -1.000000000000000000 ) ) ;
#4746=CARTESIAN_POINT ( 'NONE',  ( -0.02000000000000000042, -1.906060000575976021, -0.2916525572568466340 ) ) ;
#4772=ORIENTED_EDGE ( 'NONE', *, *, #31535, .F. ) ;
#4796=CARTESIAN_POINT ( 'NONE',  ( -0.02000000000000000042, -2.183180860297908144, -0.4937760292030871079 ) ) ;
#4815=EDGE_LOOP ( 'NONE', ( #40479, #39370, #37854, #24595, #6464 ) ) ;
#4835=FACE_OUTER_BOUND ( 'NONE', #14296, .T. ) ;
#4848=CARTESIAN_POINT ( 'NONE',  ( -0.08000000000000000167, -2.183180860297908144, -0.4937760292030871079 ) ) ;
#4882=ADVANCED_FACE ( 'NONE', ( #34632 ), #111, .T. ) ;
#4938=ORIENTED_EDGE ( 'NONE', *, *, #18179, .T. ) ;
#4960=CARTESIAN_POINT ( 'NONE',  ( -0.05464101615137761936, -2.058305985490972212, -0.5970033804171128722 ) ) ;
#4979=VECTOR ( 'NONE', #29168, 39.37007874015748854 ) ;
#5027=CARTESIAN_POINT ( 'NONE',  ( -0.02000000000000000042, -1.951160786456441754, -0.2520808614002822412 ) ) ;
#5046=CARTESIAN_POINT ( 'NONE',  ( -0.02000000000000000042, -2.200964426145791464, -1.002314564012858566 ) ) ;
#5057=VERTEX_POINT ( 'NONE', #7445 ) ;
#5062=ORIENTED_EDGE ( 'NONE', *, *, #18590, .F. ) ;
#5068=DIRECTION ( 'NONE',  ( 0.000000000000000000, 0.8063205929144885431, -0.5914787413272156735 ) ) ;
#5092=ADVANCED_FACE ( 'NONE', ( #32340 ), #35433, .F. ) ;
#5130=CARTESIAN_POINT ( 'NONE',  ( -0.02000000000000000042, -1.765869171405739957, -0.8132390237819782097 ) ) ;
#5177=VERTEX_POINT ( 'NONE', #1065 ) ;
#5189=ADVANCED_FACE ( 'NONE', ( #3706 ), #10960, .F. ) ;
#5212=ADVANCED_FACE ( 'NONE', ( #37858 ), #28989, .F. ) ;
#5227=LINE ( 'NONE', #17386, #9381 ) ;
#5285=ORIENTED_EDGE ( 'NONE', *, *, #3996, .T. ) ;
#5293=ORIENTED_EDGE ( 'NONE', *, *, #6869, .T. ) ;
#5294=ORIENTED_EDGE ( 'NONE', *, *, #39382, .F. ) ;
#5296=DIRECTION ( 'NONE',  ( 0.000000000000000000, 0.000000000000000000, -1.000000000000000000 ) ) ;
#5303=DIRECTION ( 'NONE',  ( -1.000000000000000000, -0.000000000000000000, -0.000000000000000000 ) ) ;
#5310=APPLICATION_CONTEXT ( 'configuration controlled 3d designs of mechanical parts and assemblies' ) ;
#5313=VERTEX_POINT ( 'NONE', #35777 ) ;
#5316=CARTESIAN_POINT ( 'NONE',  ( -0.02000000000000000042, -2.196071624283071788, -0.8624000883860228894 ) ) ;
#5332=ADVANCED_FACE ( 'NONE', ( #7788 ), #32690, .T. ) ;
#5340=VERTEX_POINT ( 'NONE', #20162 ) ;
#5374=VECTOR ( 'NONE', #31646, 39.37007874015748854 ) ;
#5375=FACE_OUTER_BOUND ( 'NONE', #20113, .T. ) ;
#5388=ORIENTED_EDGE ( 'NONE', *, *, #1662, .F. ) ;
#5401=ORIENTED_EDGE ( 'NONE', *, *, #14696, .T. ) ;
#5406=AXIS2_PLACEMENT_3D ( 'NONE', #36345, #23822, #21130 ) ;
#5448=DIRECTION ( 'NONE',  ( -0.4999999999999981126, 0.6509737717187621397, -0.5711682313769305130 ) ) ;
#5456=ORIENTED_EDGE ( 'NONE', *, *, #13655, .F. ) ;
#5490=DIRECTION ( 'NONE',  ( 0.000000000000000000, 0.000000000000000000, 1.000000000000000000 ) ) ;
#5494=CARTESIAN_POINT ( 'NONE',  ( -0.08000000000000000167, -2.041899626011815183, -0.6359449730384926225 ) ) ;
#5539=LINE ( 'NONE', #27976, #4671 ) ;
#5550=FACE_OUTER_BOUND ( 'NONE', #16484, .T. ) ;
#5555=DIRECTION ( 'NONE',  ( 0.000000000000000000, 0.000000000000000000, -1.000000000000000000 ) ) ;
#5557=CIRCLE ( 'NONE', #10187, 0.08000000000000000167 ) ;
#5565=VECTOR ( 'NONE', #35996, 39.37007874015748143 ) ;
#5586=VECTOR ( 'NONE', #13157, 39.37007874015748854 ) ;
#5592=LINE ( 'NONE', #8889, #38834 ) ;
#5617=VERTEX_POINT ( 'NONE', #19913 ) ;
#5621=AXIS2_PLACEMENT_3D ( 'NONE', #39189, #23762, #11014 ) ;
#5628=CARTESIAN_POINT ( 'NONE',  ( -0.02000000000000000042, -2.320036485105098301, -0.4341690811493933433 ) ) ;
#5661=DIRECTION ( 'NONE',  ( 0.4220386480983009392, 0.000000000000000000, 0.9065778397420479751 ) ) ;
#5693=CARTESIAN_POINT ( 'NONE',  ( -0.02000000000000000042, -2.183180860297908144, -0.4937760292030871079 ) ) ;
#5706=DIRECTION ( 'NONE',  ( -1.000000000000000000, 0.000000000000000000, 0.000000000000000000 ) ) ;
#5707=ORIENTED_EDGE ( 'NONE', *, *, #20111, .F. ) ;
#5709=AXIS2_PLACEMENT_3D ( 'NONE', #29066, #4168, #32561 ) ;
#5748=CIRCLE ( 'NONE', #16283, 0.01999999999999927530 ) ;
#5758=DIRECTION ( 'NONE',  ( -1.000000000000000000, -0.000000000000000000, -0.000000000000000000 ) ) ;
#5771=DIRECTION ( 'NONE',  ( 0.000000000000000000, 0.000000000000000000, 1.000000000000000000 ) ) ;
#5792=ORIENTED_EDGE ( 'NONE', *, *, #11664, .F. ) ;
#5797=VERTEX_POINT ( 'NONE', #18649 ) ;
#5836=ORIENTED_EDGE ( 'NONE', *, *, #9802, .F. ) ;
#5865=DIRECTION ( 'NONE',  ( 1.000000000000000000, -0.000000000000000000, -0.000000000000000000 ) ) ;
#5869=ADVANCED_FACE ( 'NONE', ( #40458 ), #37171, .T. ) ;
#5891=CYLINDRICAL_SURFACE ( 'NONE', #28970, 0.1620173459747806799 ) ;
#5900=EDGE_LOOP ( 'NONE', ( #22797, #7537, #23343, #6978 ) ) ;
#5916=CIRCLE ( 'NONE', #30891, 0.08000000000000000167 ) ;
#5931=DIRECTION ( 'NONE',  ( -1.000000000000000000, -0.000000000000000000, -0.000000000000000000 ) ) ;
#5941=VERTEX_POINT ( 'NONE', #17385 ) ;
#5944=DIRECTION ( 'NONE',  ( 1.000000000000000000, -0.000000000000000000, -0.000000000000000000 ) ) ;
#5948=EDGE_LOOP ( 'NONE', ( #12791, #23837, #5456, #302 ) ) ;
#5952=ORIENTED_EDGE ( 'NONE', *, *, #28522, .T. ) ;
#5972=DIRECTION ( 'NONE',  ( 0.000000000000000000, 0.000000000000000000, -1.000000000000000000 ) ) ;
#5977=VECTOR ( 'NONE', #24941, 39.37007874015748143 ) ;
#5982=EDGE_CURVE ( 'NONE', #20771, #4299, #39386, .T. ) ;
#5990=CARTESIAN_POINT ( 'NONE',  ( -0.08000000000000000167, -1.706654027108509997, -0.06438491259384497567 ) ) ;
#5996=ORIENTED_EDGE ( 'NONE', *, *, #14908, .T. ) ;
#6042=ORIENTED_EDGE ( 'NONE', *, *, #10399, .T. ) ;
#6043=ORIENTED_EDGE ( 'NONE', *, *, #25118, .T. ) ;
#6049=FACE_OUTER_BOUND ( 'NONE', #19861, .T. ) ;
#6066=CARTESIAN_POINT ( 'NONE',  ( -0.05464101615137770263, -2.542046649843399564, -0.2305290188067205259 ) ) ;
#6082=LINE ( 'NONE', #30990, #253 ) ;
#6084=ORIENTED_EDGE ( 'NONE', *, *, #9391, .F. ) ;
#6123=VECTOR ( 'NONE', #17438, 39.37007874015748143 ) ;
#6130=DIRECTION ( 'NONE',  ( 0.8660254037844403729, 0.2563705595130079118, 0.4292716345334086081 ) ) ;
#6132=CARTESIAN_POINT ( 'NONE',  ( -0.08000000000000000167, -2.032088213807425880, -0.4352898549974345555 ) ) ;
#6200=CARTESIAN_POINT ( 'NONE',  ( -0.02000000000000000042, -2.320036485105098301, -0.2941690811493925528 ) ) ;
#6278=ORIENTED_EDGE ( 'NONE', *, *, #13655, .T. ) ;
#6279=EDGE_CURVE ( 'NONE', #14928, #7855, #10986, .T. ) ;
#6294=AXIS2_PLACEMENT_3D ( 'NONE', #7274, #38973, #7489 ) ;
#6297=CARTESIAN_POINT ( 'NONE',  ( -0.05464101615137770263, -2.320036485105098301, -0.2941690811493925528 ) ) ;
#6300=ORIENTED_EDGE ( 'NONE', *, *, #12169, .T. ) ;
#6313=DIRECTION ( 'NONE',  ( 0.4999999999999979461, -0.03026636220570700850, -0.8654963589286988057 ) ) ;
#6343=DIRECTION ( 'NONE',  ( -1.000000000000000000, -0.000000000000000000, -0.000000000000000000 ) ) ;
#6380=CARTESIAN_POINT ( 'NONE',  ( -0.05464101615137766793, -2.548345659627495596, -0.2263512047145338490 ) ) ;
#6404=ADVANCED_FACE ( 'NONE', ( #17129 ), #14643, .F. ) ;
#6413=DIRECTION ( 'NONE',  ( 1.000000000000000000, -0.000000000000000000, -0.000000000000000000 ) ) ;
#6421=EDGE_CURVE ( 'NONE', #28686, #17786, #39529, .T. ) ;
#6429=SHAPE_REPRESENTATION_RELATIONSHIP ( 'NONE' , 'NONE' ,  #9349, #33372 ) ;
#6439=EDGE_CURVE ( 'NONE', #28686, #7245, #12275, .T. ) ;
#6451=CARTESIAN_POINT ( 'NONE',  ( -0.08000000000000000167, -1.622350287959229087, -0.08960079202753243321 ) ) ;
#6457=CARTESIAN_POINT ( 'NONE',  ( -0.05464101615137770263, -2.183180860297908144, -0.4937760292030871079 ) ) ;
#6460=CARTESIAN_POINT ( 'NONE',  ( -0.02000000000000000042, -2.212972691094449385, -0.5913464432512408608 ) ) ;
#6461=ORIENTED_EDGE ( 'NONE', *, *, #9883, .F. ) ;
#6464=ORIENTED_EDGE ( 'NONE', *, *, #31027, .F. ) ;
#6479=FACE_BOUND ( 'NONE', #12469, .T. ) ;
#6496=DIRECTION ( 'NONE',  ( 1.000000000000000000, 0.000000000000000000, 0.000000000000000000 ) ) ;
#6533=LINE ( 'NONE', #226, #827 ) ;
#6547=ORIENTED_EDGE ( 'NONE', *, *, #30034, .T. ) ;
#6589=EDGE_LOOP ( 'NONE', ( #29954, #12841, #27071, #12966 ) ) ;
#6598=VERTEX_POINT ( 'NONE', #18146 ) ;
#6617=EDGE_CURVE ( 'NONE', #36330, #37905, #21856, .T. ) ;
#6622=( NAMED_UNIT ( * ) PLANE_ANGLE_UNIT ( ) SI_UNIT ( $, .RADIAN. ) );
#6638=EDGE_CURVE ( 'NONE', #16250, #38006, #31706, .T. ) ;
#6650=FACE_OUTER_BOUND ( 'NONE', #2673, .T. ) ;
#6665=DIRECTION ( 'NONE',  ( 1.000000000000000000, 0.000000000000000000, 0.000000000000000000 ) ) ;
#6669=CARTESIAN_POINT ( 'NONE',  ( -0.08000000000000000167, -1.546789565643408304, -0.06332195561662114225 ) ) ;
#6709=CARTESIAN_POINT ( 'NONE',  ( -0.05464101615137785528, -2.631664041040912227, -0.5119035495255163104 ) ) ;
#6716=ORIENTED_EDGE ( 'NONE', *, *, #8003, .F. ) ;
#6774=ORIENTED_EDGE ( 'NONE', *, *, #1200, .T. ) ;
#6778=CIRCLE ( 'NONE', #2854, 0.4488493849861018292 ) ;
#6804=ORIENTED_EDGE ( 'NONE', *, *, #37694, .T. ) ;
#6810=ORIENTED_EDGE ( 'NONE', *, *, #20367, .T. ) ;
#6827=DIRECTION ( 'NONE',  ( 0.000000000000000000, 1.951319995474460317E-15, -1.000000000000000000 ) ) ;
#6846=CIRCLE ( 'NONE', #36438, 0.08000000000000000167 ) ;
#6863=DIRECTION ( 'NONE',  ( 0.000000000000000000, 0.000000000000000000, -1.000000000000000000 ) ) ;
#6867=ORIENTED_EDGE ( 'NONE', *, *, #10577, .F. ) ;
#6869=EDGE_CURVE ( 'NONE', #18110, #37905, #23488, .T. ) ;
#6901=LINE ( 'NONE', #31812, #36465 ) ;
#6916=CARTESIAN_POINT ( 'NONE',  ( -0.02000000000000000042, -1.758704040287260018, -0.8825853814972600686 ) ) ;
#6923=CARTESIAN_POINT ( 'NONE',  ( -0.02000000000000000042, -2.196071624283071788, -0.8624000883860228894 ) ) ;
#6932=DIRECTION ( 'NONE',  ( -1.000000000000000000, -0.000000000000000000, -0.000000000000000000 ) ) ;
#6938=ADVANCED_FACE ( 'NONE', ( #8225 ), #36136, .F. ) ;
#6943=AXIS2_PLACEMENT_3D ( 'NONE', #33028, #24002, #33239 ) ;
#6969=CARTESIAN_POINT ( 'NONE',  ( -0.05464101615137771650, -2.698373762442814350, -0.2370085142459261163 ) ) ;
#6976=ORIENTED_EDGE ( 'NONE', *, *, #6617, .T. ) ;
#6977=DIRECTION ( 'NONE',  ( 0.4220386480983009392, 0.000000000000000000, -0.9065778397420479751 ) ) ;
#6978=ORIENTED_EDGE ( 'NONE', *, *, #3996, .F. ) ;
#6992=LINE ( 'NONE', #28613, #28604 ) ;
#6996=EDGE_CURVE ( 'NONE', #5340, #2068, #24093, .T. ) ;
#7020=CARTESIAN_POINT ( 'NONE',  ( -0.02000000000000000042, -2.177105168660885326, -0.2518349584362399862 ) ) ;
#7022=EDGE_CURVE ( 'NONE', #22988, #2067, #5539, .T. ) ;
#7060=AXIS2_PLACEMENT_3D ( 'NONE', #6457, #19230, #560 ) ;
#7092=DIRECTION ( 'NONE',  ( 0.000000000000000000, 0.000000000000000000, -1.000000000000000000 ) ) ;
#7120=ORIENTED_EDGE ( 'NONE', *, *, #36389, .T. ) ;
#7123=ORIENTED_EDGE ( 'NONE', *, *, #21287, .T. ) ;
#7127=PRODUCT_DEFINITION_SHAPE ( 'NONE', 'NONE',  #35536 ) ;
#7128=DIRECTION ( 'NONE',  ( 0.000000000000000000, 0.000000000000000000, 1.000000000000000000 ) ) ;
#7136=FACE_OUTER_BOUND ( 'NONE', #25976, .T. ) ;
#7149=DIRECTION ( 'NONE',  ( -1.000000000000000000, 0.000000000000000000, 0.000000000000000000 ) ) ;
#7174=CYLINDRICAL_SURFACE ( 'NONE', #19365, 0.1620173459747806799 ) ;
#7185=EDGE_CURVE ( 'NONE', #10881, #13458, #3874, .T. ) ;
#7187=ADVANCED_FACE ( 'NONE', ( #16035 ), #16425, .F. ) ;
#7194=CARTESIAN_POINT ( 'NONE',  ( -0.05464101615137768181, -2.367354784411275670, -0.3586747285825516718 ) ) ;
#7203=LINE ( 'NONE', #897, #4006 ) ;
#7210=EDGE_CURVE ( 'NONE', #36294, #20037, #5916, .T. ) ;
#7227=FACE_BOUND ( 'NONE', #4479, .T. ) ;
#7240=ORIENTED_EDGE ( 'NONE', *, *, #13433, .T. ) ;
#7243=AXIS2_PLACEMENT_3D ( 'NONE', #12851, #25815, #34447 ) ;
#7245=VERTEX_POINT ( 'NONE', #21908 ) ;
#7253=VERTEX_POINT ( 'NONE', #13044 ) ;
#7274=CARTESIAN_POINT ( 'NONE',  ( -0.05464101615137773038, -2.626773565144302935, -0.2726934094652516127 ) ) ;
#7275=VECTOR ( 'NONE', #34343, 39.37007874015748143 ) ;
#7291=DIRECTION ( 'NONE',  ( 0.000000000000000000, 0.000000000000000000, 1.000000000000000000 ) ) ;
#7293=AXIS2_PLACEMENT_3D ( 'NONE', #33640, #24819, #30770 ) ;
#7308=CARTESIAN_POINT ( 'NONE',  ( -0.02000000000000000042, -2.067054404790649613, -0.8080442508481435748 ) ) ;
#7317=LINE ( 'NONE', #23202, #15574 ) ;
#7319=VERTEX_POINT ( 'NONE', #2767 ) ;
#7366=DIRECTION ( 'NONE',  ( -1.000000000000000000, -0.000000000000000000, -0.000000000000000000 ) ) ;
#7367=EDGE_CURVE ( 'NONE', #23493, #12543, #25735, .T. ) ;
#7376=CIRCLE ( 'NONE', #23155, 0.06250000000000001388 ) ;
#7393=CARTESIAN_POINT ( 'NONE',  ( -0.02000000000000000042, -1.599201040860868339, 0.1642182323853691728 ) ) ;
#7401=CARTESIAN_POINT ( 'NONE',  ( -0.02000000000000000042, -2.551729310907437043, -0.5086726180052709712 ) ) ;
#7404=VECTOR ( 'NONE', #3299, 39.37007874015748854 ) ;
#7438=CIRCLE ( 'NONE', #30449, 0.6443128707267505861 ) ;
#7441=VECTOR ( 'NONE', #39039, 39.37007874015748143 ) ;
#7445=CARTESIAN_POINT ( 'NONE',  ( -0.08000000000000000167, -1.758704040287259573, -0.8825853814972599576 ) ) ;
#7454=ORIENTED_EDGE ( 'NONE', *, *, #23993, .F. ) ;
#7464=AXIS2_PLACEMENT_3D ( 'NONE', #39249, #17835, #35962 ) ;
#7466=AXIS2_PLACEMENT_3D ( 'NONE', #8507, #21281, #2747 ) ;
#7481=ORIENTED_EDGE ( 'NONE', *, *, #7022, .F. ) ;
#7485=DIRECTION ( 'NONE',  ( 1.000000000000000000, 0.000000000000000000, 0.000000000000000000 ) ) ;
#7489=DIRECTION ( 'NONE',  ( 0.000000000000000000, 0.000000000000000000, -1.000000000000000000 ) ) ;
#7508=ORIENTED_EDGE ( 'NONE', *, *, #27330, .T. ) ;
#7516=CARTESIAN_POINT ( 'NONE',  ( -0.05464101615137763324, -2.183180860297908144, -0.4937760292030871079 ) ) ;
#7518=CARTESIAN_POINT ( 'NONE',  ( -0.02000000000000000042, -1.802948570736253586, -0.8420585814095631338 ) ) ;
#7537=ORIENTED_EDGE ( 'NONE', *, *, #33934, .T. ) ;
#7553=AXIS2_PLACEMENT_3D ( 'NONE', #29819, #10685, #13764 ) ;
#7633=ORIENTED_EDGE ( 'NONE', *, *, #34025, .F. ) ;
#7663=VECTOR ( 'NONE', #6932, 39.37007874015748143 ) ;
#7666=EDGE_CURVE ( 'NONE', #24008, #11393, #30229, .T. ) ;
#7713=CARTESIAN_POINT ( 'NONE',  ( -0.02000000000000000042, -2.468922287121626091, -0.3957877349972418468 ) ) ;
#7724=DIRECTION ( 'NONE',  ( -0.4999999999999965028, -0.6509737717187625838, 0.5711682313769312902 ) ) ;
#7775=EDGE_LOOP ( 'NONE', ( #32510, #24118, #38842, #28894, #26875 ) ) ;
#7788=FACE_OUTER_BOUND ( 'NONE', #38636, .T. ) ;
#7802=DIRECTION ( 'NONE',  ( 1.000000000000000000, 0.000000000000000000, 0.000000000000000000 ) ) ;
#7812=ORIENTED_EDGE ( 'NONE', *, *, #2958, .F. ) ;
#7829=ORIENTED_EDGE ( 'NONE', *, *, #19808, .T. ) ;
#7830=ORIENTED_EDGE ( 'NONE', *, *, #6421, .T. ) ;
#7855=VERTEX_POINT ( 'NONE', #36206 ) ;
#7866=VERTEX_POINT ( 'NONE', #1879 ) ;
#7869=CONICAL_SURFACE ( 'NONE', #38103, 0.5543128707267515054, 1.047197551196601628 ) ;
#7871=VERTEX_POINT ( 'NONE', #24101 ) ;
#7915=DIRECTION ( 'NONE',  ( 0.000000000000000000, 0.000000000000000000, -1.000000000000000000 ) ) ;
#7918=DIRECTION ( 'NONE',  ( 0.000000000000000000, 3.557598251760403443E-15, -1.000000000000000000 ) ) ;
#7921=DIRECTION ( 'NONE',  ( -1.000000000000000000, -0.000000000000000000, -0.000000000000000000 ) ) ;
#7950=CIRCLE ( 'NONE', #32273, 0.1400000000000009570 ) ;
#7951=ADVANCED_FACE ( 'NONE', ( #18931 ), #27572, .F. ) ;
#7954=CARTESIAN_POINT ( 'NONE',  ( -0.02000000000000000042, -2.631664041040912227, -0.5119035495255163104 ) ) ;
#7971=AXIS2_PLACEMENT_3D ( 'NONE', #32010, #9180, #21036 ) ;
#7978=CARTESIAN_POINT ( 'NONE',  ( -0.02000000000000000042, -1.598492537578166672, -0.1971380022280825872 ) ) ;
#7994=DIRECTION ( 'NONE',  ( 1.000000000000000000, 0.000000000000000000, 0.000000000000000000 ) ) ;
#8003=EDGE_CURVE ( 'NONE', #26509, #22200, #30914, .T. ) ;
#8008=DIRECTION ( 'NONE',  ( 1.000000000000000000, 0.000000000000000000, 0.000000000000000000 ) ) ;
#8012=DIRECTION ( 'NONE',  ( -1.000000000000000000, -0.000000000000000000, -0.000000000000000000 ) ) ;
#8025=AXIS2_PLACEMENT_3D ( 'NONE', #19192, #28057, #6827 ) ;
#8027=ORIENTED_EDGE ( 'NONE', *, *, #12011, .T. ) ;
#8035=ORIENTED_EDGE ( 'NONE', *, *, #12984, .F. ) ;
#8048=DIRECTION ( 'NONE',  ( 0.4697114767686426107, -0.8828199865158358195, 0.000000000000000000 ) ) ;
#8053=DIRECTION ( 'NONE',  ( 1.000000000000000000, 0.000000000000000000, 0.000000000000000000 ) ) ;
#8065=VECTOR ( 'NONE', #25894, 39.37007874015748854 ) ;
#8080=LINE ( 'NONE', #32975, #1626 ) ;
#8089=AXIS2_PLACEMENT_3D ( 'NONE', #4280, #10657, #22836 ) ;
#8177=AXIS2_PLACEMENT_3D ( 'NONE', #39894, #11713, #3074 ) ;
#8178=EDGE_LOOP ( 'NONE', ( #25717, #11280, #7454, #1481 ) ) ;
#8218=AXIS2_PLACEMENT_3D ( 'NONE', #16017, #1025, #435 ) ;
#8220=EDGE_CURVE ( 'NONE', #22200, #20037, #16855, .T. ) ;
#8225=FACE_OUTER_BOUND ( 'NONE', #7775, .T. ) ;
#8234=VECTOR ( 'NONE', #20832, 39.37007874015748854 ) ;
#8237=EDGE_LOOP ( 'NONE', ( #4520, #7508, #21828, #4489 ) ) ;
#8265=AXIS2_PLACEMENT_3D ( 'NONE', #28323, #37575, #197 ) ;
#8308=EDGE_LOOP ( 'NONE', ( #3710, #13049, #14054, #15085 ) ) ;
#8315=DIRECTION ( 'NONE',  ( 1.000000000000000000, 0.000000000000000000, 0.000000000000000000 ) ) ;
#8322=CARTESIAN_POINT ( 'NONE',  ( -0.05464101615137796630, -1.682484669133182953, -0.03683853088544701559 ) ) ;
#8346=ORIENTED_EDGE ( 'NONE', *, *, #1657, .F. ) ;
#8353=LINE ( 'NONE', #36938, #30315 ) ;
#8363=PLANE ( 'NONE',  #33857 ) ;
#8403=LINE ( 'NONE', #20973, #35603 ) ;
#8411=CARTESIAN_POINT ( 'NONE',  ( -0.02000000000000000042, -2.551729310907437043, -0.5086726180052709712 ) ) ;
#8416=DIRECTION ( 'NONE',  ( 0.000000000000000000, 0.000000000000000000, -1.000000000000000000 ) ) ;
#8437=EDGE_LOOP ( 'NONE', ( #27492, #34837, #34760, #16247 ) ) ;
#8444=ORIENTED_EDGE ( 'NONE', *, *, #10314, .T. ) ;
#8451=LINE ( 'NONE', #4960, #2148 ) ;
#8477=CARTESIAN_POINT ( 'NONE',  ( -0.02000000000000000042, -1.699711333021935777, -0.9366211149475224262 ) ) ;
#8485=ORIENTED_EDGE ( 'NONE', *, *, #24647, .T. ) ;
#8507=CARTESIAN_POINT ( 'NONE',  ( -0.05464101615137796630, -2.070343076906777213, -0.2454056712452573896 ) ) ;
#8526=VERTEX_POINT ( 'NONE', #24854 ) ;
#8542=DIRECTION ( 'NONE',  ( 0.4999999999999982792, 0.6404870708789264233, -0.5829033470798866690 ) ) ;
#8550=LINE ( 'NONE', #12064, #9341 ) ;
#8562=FACE_OUTER_BOUND ( 'NONE', #16304, .T. ) ;
#8592=ORIENTED_EDGE ( 'NONE', *, *, #13765, .T. ) ;
#8600=PLANE ( 'NONE',  #4113 ) ;
#8623=ADVANCED_FACE ( 'NONE', ( #27333 ), #5891, .T. ) ;
#8629=CYLINDRICAL_SURFACE ( 'NONE', #17269, 0.08000000000000000167 ) ;
#8655=DIRECTION ( 'NONE',  ( -1.000000000000000000, 0.000000000000000000, 0.000000000000000000 ) ) ;
#8668=CIRCLE ( 'NONE', #8025, 0.1400000000000009570 ) ;
#8675=EDGE_CURVE ( 'NONE', #8899, #641, #11882, .T. ) ;
#8697=EDGE_CURVE ( 'NONE', #35302, #14209, #23097, .T. ) ;
#8699=AXIS2_PLACEMENT_3D ( 'NONE', #1311, #13817, #14025 ) ;
#8714=AXIS2_PLACEMENT_3D ( 'NONE', #434, #9634, #7128 ) ;
#8744=VERTEX_POINT ( 'NONE', #12903 ) ;
#8764=VECTOR ( 'NONE', #31858, 39.37007874015748143 ) ;
#8776=CONICAL_SURFACE ( 'NONE', #37024, 0.1400000000000009570, 1.047197551196600962 ) ;
#8808=VERTEX_POINT ( 'NONE', #11430 ) ;
#8814=CARTESIAN_POINT ( 'NONE',  ( -0.02000000000000000042, -2.183180860297908144, -0.4937760292030871079 ) ) ;
#8815=AXIS2_PLACEMENT_3D ( 'NONE', #37494, #9316, #25172 ) ;
#8855=CONICAL_SURFACE ( 'NONE', #35787, 0.1400000000000009570, 1.047197551196600962 ) ;
#8857=ORIENTED_EDGE ( 'NONE', *, *, #35356, .T. ) ;
#8889=CARTESIAN_POINT ( 'NONE',  ( -0.05464101615137761936, -1.984114763688379579, -0.7731012124309359912 ) ) ;
#8899=VERTEX_POINT ( 'NONE', #1582 ) ;
#8913=CYLINDRICAL_SURFACE ( 'NONE', #34440, 0.06250000000000001388 ) ;
#8916=CARTESIAN_POINT ( 'NONE',  ( -0.05464101615137796630, -1.622350287959229087, -0.08960079202753243321 ) ) ;
#8920=CARTESIAN_POINT ( 'NONE',  ( 0.000000000000000000, 0.000000000000000000, 0.000000000000000000 ) ) ;
#8929=FACE_OUTER_BOUND ( 'NONE', #29732, .T. ) ;
#8934=EDGE_LOOP ( 'NONE', ( #562, #26270, #4397, #6867 ) ) ;
#8964=ORIENTED_EDGE ( 'NONE', *, *, #23876, .F. ) ;
#8976=VECTOR ( 'NONE', #21034, 39.37007874015748143 ) ;
#9006=PLANE ( 'NONE',  #33765 ) ;
#9010=ORIENTED_EDGE ( 'NONE', *, *, #12935, .T. ) ;
#9033=DIRECTION ( 'NONE',  ( 1.000000000000000000, -0.000000000000000000, -0.000000000000000000 ) ) ;
#9046=CIRCLE ( 'NONE', #7060, 0.1620173459747806799 ) ;
#9068=DIRECTION ( 'NONE',  ( 0.4999999999999968359, -0.4440468346413921075, -0.7435202812600091304 ) ) ;
#9141=DIRECTION ( 'NONE',  ( 0.4999999999999970024, 0.2529028965469328760, 0.8282753919549792343 ) ) ;
#9164=CARTESIAN_POINT ( 'NONE',  ( -0.08000000000000000167, -2.183180860297908144, -0.4937760292030871079 ) ) ;
#9180=DIRECTION ( 'NONE',  ( -1.000000000000000000, 0.000000000000000000, 0.000000000000000000 ) ) ;
#9181=DIRECTION ( 'NONE',  ( 0.000000000000000000, 0.000000000000000000, -1.000000000000000000 ) ) ;
#9195=EDGE_CURVE ( 'NONE', #1840, #641, #2083, .T. ) ;
#9205=ORIENTED_EDGE ( 'NONE', *, *, #25007, .F. ) ;
#9217=CARTESIAN_POINT ( 'NONE',  ( -0.08000000000000000167, -2.179113517810423062, -0.3318097452986852880 ) ) ;
#9233=CARTESIAN_POINT ( 'NONE',  ( -0.02000000000000000042, -2.274798198814180772, -0.3601501197397404264 ) ) ;
#9273=CARTESIAN_POINT ( 'NONE',  ( -0.08000000000000000167, -1.518907846805490403, -0.1889969338327479598 ) ) ;
#9285=AXIS2_PLACEMENT_3D ( 'NONE', #39221, #7921, #20497 ) ;
#9294=VECTOR ( 'NONE', #9516, 39.37007874015748143 ) ;
#9300=DIRECTION ( 'NONE',  ( 0.000000000000000000, 0.000000000000000000, 1.000000000000000000 ) ) ;
#9316=DIRECTION ( 'NONE',  ( -1.000000000000000000, -0.000000000000000000, -0.000000000000000000 ) ) ;
#9320=CONICAL_SURFACE ( 'NONE', #21835, 0.1620173459747806799, 1.047197551196600518 ) ;
#9335=ORIENTED_EDGE ( 'NONE', *, *, #29419, .F. ) ;
#9341=VECTOR ( 'NONE', #24628, 39.37007874015748143 ) ;
#9345=ORIENTED_EDGE ( 'NONE', *, *, #22368, .T. ) ;
#9349=SHAPE_REPRESENTATION ( 'Outer shift plate', ( #27819 ), #3510 ) ;
#9365=DIRECTION ( 'NONE',  ( 0.000000000000000000, 0.000000000000000000, -1.000000000000000000 ) ) ;
#9381=VECTOR ( 'NONE', #27269, 39.37007874015748854 ) ;
#9391=EDGE_CURVE ( 'NONE', #8526, #30280, #14454, .T. ) ;
#9410=VECTOR ( 'NONE', #39383, 39.37007874015748143 ) ;
#9415=VERTEX_POINT ( 'NONE', #12812 ) ;
#9423=CARTESIAN_POINT ( 'NONE',  ( -0.05464101615137761936, -1.845925619402022155, -0.3444148183989317880 ) ) ;
#9424=ADVANCED_FACE ( 'NONE', ( #37692 ), #9320, .T. ) ;
#9484=EDGE_CURVE ( 'NONE', #18990, #38792, #14578, .T. ) ;
#9485=CARTESIAN_POINT ( 'NONE',  ( -0.05464101615137773038, -1.659335422034822205, 0.2169804935274543545 ) ) ;
#9487=LINE ( 'NONE', #12782, #17231 ) ;
#9516=DIRECTION ( 'NONE',  ( 0.000000000000000000, -0.6595282642760668113, -0.7516797646744246553 ) ) ;
#9563=ORIENTED_EDGE ( 'NONE', *, *, #15020, .T. ) ;
#9572=DIRECTION ( 'NONE',  ( 0.000000000000000000, 0.000000000000000000, -1.000000000000000000 ) ) ;
#9624=ORIENTED_EDGE ( 'NONE', *, *, #216, .F. ) ;
#9628=ORIENTED_EDGE ( 'NONE', *, *, #19319, .T. ) ;
#9634=DIRECTION ( 'NONE',  ( -1.000000000000000000, 0.000000000000000000, 0.000000000000000000 ) ) ;
#9702=DIRECTION ( 'NONE',  ( -0.000000000000000000, -0.6595282642760673664, -0.7516797646744242112 ) ) ;
#9723=CARTESIAN_POINT ( 'NONE',  ( -0.02000000000000000042, -2.183180860297908144, -0.5562760292030870524 ) ) ;
#9732=( LENGTH_UNIT ( ) NAMED_UNIT ( * ) SI_UNIT ( $, .METRE. ) );
#9741=DIRECTION ( 'NONE',  ( 0.000000000000000000, 0.3882559824134195758, -0.9215515678030125057 ) ) ;
#9747=ORIENTED_EDGE ( 'NONE', *, *, #20572, .F. ) ;
#9751=ORIENTED_EDGE ( 'NONE', *, *, #35938, .F. ) ;
#9755=FACE_OUTER_BOUND ( 'NONE', #8934, .T. ) ;
#9772=DIRECTION ( 'NONE',  ( 0.4999999999999972800, -0.5122356157878119598, -0.6982941170584811008 ) ) ;
#9776=PLANE ( 'NONE',  #26451 ) ;
#9802=EDGE_CURVE ( 'NONE', #20865, #10794, #39314, .T. ) ;
#9818=ORIENTED_EDGE ( 'NONE', *, *, #23072, .T. ) ;
#9826=FACE_OUTER_BOUND ( 'NONE', #32731, .T. ) ;
#9829=DIRECTION ( 'NONE',  ( 1.000000000000000000, -0.000000000000000000, -0.000000000000000000 ) ) ;
#9831=LINE ( 'NONE', #6132, #5374 ) ;
#9839=DIRECTION ( 'NONE',  ( -0.4999999999999962808, 0.6386147891223726836, -0.5849539735006431540 ) ) ;
#9851=CARTESIAN_POINT ( 'NONE',  ( -0.02000000000000000042, -2.177105168660885326, -0.2518349584362399862 ) ) ;
#9857=CARTESIAN_POINT ( 'NONE',  ( -0.02000000000000000042, -2.263760933879813919, -0.5090783786781539755 ) ) ;
#9883=EDGE_CURVE ( 'NONE', #14004, #4299, #26788, .T. ) ;
#9903=VECTOR ( 'NONE', #11606, 39.37007874015748854 ) ;
#9917=LINE ( 'NONE', #9723, #106 ) ;
#9931=CARTESIAN_POINT ( 'NONE',  ( -0.02000000000000000042, -1.646519645934556131, -0.1171471737359304072 ) ) ;
#9940=AXIS2_PLACEMENT_3D ( 'NONE', #39886, #2253, #5296 ) ;
#9944=VERTEX_POINT ( 'NONE', #40324 ) ;
#9955=CARTESIAN_POINT ( 'NONE',  ( -0.02000000000000000042, -2.626773565144302935, -0.2726934094652516127 ) ) ;
#9965=ORIENTED_EDGE ( 'NONE', *, *, #21741, .T. ) ;
#10011=AXIS2_PLACEMENT_3D ( 'NONE', #6451, #19022, #30950 ) ;
#10013=LINE ( 'NONE', #6916, #19369 ) ;
#10041=LINE ( 'NONE', #32655, #4979 ) ;
#10051=DIRECTION ( 'NONE',  ( -0.000000000000000000, 0.9215515678030125057, 0.3882559824134196313 ) ) ;
#10095=AXIS2_PLACEMENT_3D ( 'NONE', #9851, #5944, #38039 ) ;
#10101=VECTOR ( 'NONE', #843, 39.37007874015748143 ) ;
#10107=CIRCLE ( 'NONE', #18653, 0.1400000000000003464 ) ;
#10115=VERTEX_POINT ( 'NONE', #23653 ) ;
#10117=DIRECTION ( 'NONE',  ( 0.000000000000000000, 0.000000000000000000, -1.000000000000000000 ) ) ;
#10187=AXIS2_PLACEMENT_3D ( 'NONE', #21208, #12353, #5555 ) ;
#10193=EDGE_CURVE ( 'NONE', #25764, #20672, #8668, .T. ) ;
#10197=DIRECTION ( 'NONE',  ( 0.000000000000000000, 0.000000000000000000, -1.000000000000000000 ) ) ;
#10214=CYLINDRICAL_SURFACE ( 'NONE', #34260, 0.5756329413417605734 ) ;
#10242=EDGE_CURVE ( 'NONE', #2236, #18399, #23517, .T. ) ;
#10254=CARTESIAN_POINT ( 'NONE',  ( -0.05464101615137786222, -2.196071624283071788, -0.8624000883860228894 ) ) ;
#10294=DIRECTION ( 'NONE',  ( 0.000000000000000000, 0.000000000000000000, -1.000000000000000000 ) ) ;
#10314=EDGE_CURVE ( 'NONE', #27272, #7871, #17230, .T. ) ;
#10318=ORIENTED_EDGE ( 'NONE', *, *, #3164, .F. ) ;
#10324=FACE_OUTER_BOUND ( 'NONE', #31664, .T. ) ;
#10332=CARTESIAN_POINT ( 'NONE',  ( -0.08000000000000000167, -2.183180860297908144, -0.4937760292030871079 ) ) ;
#10368=CONICAL_SURFACE ( 'NONE', #22223, 0.1400000000000007627, 1.047197551196601406 ) ;
#10371=ORIENTED_EDGE ( 'NONE', *, *, #11488, .F. ) ;
#10380=DIRECTION ( 'NONE',  ( 0.000000000000000000, 0.000000000000000000, -1.000000000000000000 ) ) ;
#10399=EDGE_CURVE ( 'NONE', #16250, #32357, #7376, .T. ) ;
#10405=EDGE_CURVE ( 'NONE', #30911, #14004, #8451, .T. ) ;
#10428=ORIENTED_EDGE ( 'NONE', *, *, #1226, .F. ) ;
#10437=LINE ( 'NONE', #16610, #8065 ) ;
#10443=CARTESIAN_POINT ( 'NONE',  ( -0.08000000000000000167, -2.180132361182266720, -0.6941833704005058170 ) ) ;
#10452=EDGE_CURVE ( 'NONE', #19821, #16708, #38894, .T. ) ;
#10454=CARTESIAN_POINT ( 'NONE',  ( -0.02000000000000000042, -2.183180860297908144, -0.4937760292030871079 ) ) ;
#10460=ORIENTED_EDGE ( 'NONE', *, *, #10193, .F. ) ;
#10508=DIRECTION ( 'NONE',  ( -1.000000000000000000, -0.000000000000000000, -0.000000000000000000 ) ) ;
#10510=ORIENTED_EDGE ( 'NONE', *, *, #39691, .T. ) ;
#10523=EDGE_LOOP ( 'NONE', ( #15605, #28554, #34995, #18685 ) ) ;
#10560=DIRECTION ( 'NONE',  ( 0.000000000000000000, 0.000000000000000000, 1.000000000000000000 ) ) ;
#10565=AXIS2_PLACEMENT_3D ( 'NONE', #3333, #25378, #31345 ) ;
#10567=ORIENTED_EDGE ( 'NONE', *, *, #662, .F. ) ;
#10577=EDGE_CURVE ( 'NONE', #4305, #35302, #15910, .T. ) ;
#10625=AXIS2_PLACEMENT_3D ( 'NONE', #22366, #6496, #19274 ) ;
#10627=DIRECTION ( 'NONE',  ( -0.000000000000000000, -0.6595282642760672553, -0.7516797646744243222 ) ) ;
#10657=DIRECTION ( 'NONE',  ( -1.000000000000000000, -0.000000000000000000, -0.000000000000000000 ) ) ;
#10658=FACE_OUTER_BOUND ( 'NONE', #34950, .T. ) ;
#10685=DIRECTION ( 'NONE',  ( -1.000000000000000000, -0.000000000000000000, -0.000000000000000000 ) ) ;
#10690=ADVANCED_FACE ( 'NONE', ( #7136 ), #34729, .T. ) ;
#10692=EDGE_CURVE ( 'NONE', #12973, #27138, #32053, .T. ) ;
#10711=AXIS2_PLACEMENT_3D ( 'NONE', #3680, #10051, #28575 ) ;
#10724=CONICAL_SURFACE ( 'NONE', #14646, 0.1400000000000013733, 1.047197551196602294 ) ;
#10731=ORIENTED_EDGE ( 'NONE', *, *, #16039, .F. ) ;
#10737=CARTESIAN_POINT ( 'NONE',  ( -0.02000000000000000042, -2.691615088641019504, -0.5143267481657003426 ) ) ;
#10747=DIRECTION ( 'NONE',  ( 0.000000000000000000, 0.000000000000000000, -1.000000000000000000 ) ) ;
#10748=DIRECTION ( 'NONE',  ( 0.000000000000000000, 0.000000000000000000, 1.000000000000000000 ) ) ;
#10754=DIRECTION ( 'NONE',  ( 1.000000000000000000, 0.000000000000000000, 0.000000000000000000 ) ) ;
#10790=CIRCLE ( 'NONE', #20601, 0.1400000000000013178 ) ;
#10794=VERTEX_POINT ( 'NONE', #23217 ) ;
#10801=AXIS2_PLACEMENT_3D ( 'NONE', #13463, #13053, #6863 ) ;
#10807=CONICAL_SURFACE ( 'NONE', #40371, 0.6443128707267505861, 1.047197551196601184 ) ;
#10861=VECTOR ( 'NONE', #15942, 39.37007874015748143 ) ;
#10863=VECTOR ( 'NONE', #26286, 39.37007874015748143 ) ;
#10867=CARTESIAN_POINT ( 'NONE',  ( -0.02000000000000000042, -1.910390638264138685, -0.7420407338378623985 ) ) ;
#10871=DIRECTION ( 'NONE',  ( -1.000000000000000000, 0.000000000000000000, 0.000000000000000000 ) ) ;
#10878=VERTEX_POINT ( 'NONE', #10443 ) ;
#10881=VERTEX_POINT ( 'NONE', #38623 ) ;
#10908=CARTESIAN_POINT ( 'NONE',  ( -0.02000000000000000042, -2.218388099582461415, -0.4932950115394270085 ) ) ;
#10915=DIRECTION ( 'NONE',  ( 0.000000000000000000, 0.000000000000000000, -1.000000000000000000 ) ) ;
#10920=AXIS2_PLACEMENT_3D ( 'NONE', #25938, #22435, #32085 ) ;
#10955=ADVANCED_FACE ( 'NONE', ( #39430 ), #12668, .F. ) ;
#10960=CONICAL_SURFACE ( 'NONE', #16861, 0.1400000000000004297, 1.047197551196599630 ) ;
#10962=DIRECTION ( 'NONE',  ( -1.000000000000000000, -0.000000000000000000, -0.000000000000000000 ) ) ;
#10967=LENGTH_MEASURE_WITH_UNIT ( LENGTH_MEASURE( 0.02539999999999999897 ), #38919 );
#10986=CIRCLE ( 'NONE', #5709, 0.08000000000000000167 ) ;
#11014=DIRECTION ( 'NONE',  ( 0.000000000000000000, 6.829619984160658243E-15, -1.000000000000000000 ) ) ;
#11043=DIRECTION ( 'NONE',  ( 1.000000000000000000, -0.000000000000000000, -0.000000000000000000 ) ) ;
#11053=CIRCLE ( 'NONE', #36676, 0.08000000000000002942 ) ;
#11083=ORIENTED_EDGE ( 'NONE', *, *, #4642, .T. ) ;
#11120=EDGE_LOOP ( 'NONE', ( #12339, #15232, #7240, #14315 ) ) ;
#11130=DIRECTION ( 'NONE',  ( -1.000000000000000000, -0.000000000000000000, -0.000000000000000000 ) ) ;
#11160=DIRECTION ( 'NONE',  ( -1.000000000000000000, -0.000000000000000000, -0.000000000000000000 ) ) ;
#11164=ORIENTED_EDGE ( 'NONE', *, *, #38802, .F. ) ;
#11176=CARTESIAN_POINT ( 'NONE',  ( -0.02000000000000000042, -2.039246558356380135, -0.5681570558249129377 ) ) ;
#11194=CARTESIAN_POINT ( 'NONE',  ( -0.08000000000000000167, -2.379949255320110257, -0.6346823614705312533 ) ) ;
#11195=ADVANCED_FACE ( 'NONE', ( #23274 ), #14589, .F. ) ;
#11220=DIRECTION ( 'NONE',  ( -1.000000000000000000, -0.000000000000000000, -0.000000000000000000 ) ) ;
#11228=DIRECTION ( 'NONE',  ( 0.000000000000000000, 0.000000000000000000, -1.000000000000000000 ) ) ;
#11235=EDGE_LOOP ( 'NONE', ( #20083, #32301, #12049, #19923 ) ) ;
#11247=EDGE_CURVE ( 'NONE', #21046, #24008, #19239, .T. ) ;
#11266=DIRECTION ( 'NONE',  ( 0.000000000000000000, 0.000000000000000000, -1.000000000000000000 ) ) ;
#11280=ORIENTED_EDGE ( 'NONE', *, *, #34264, .F. ) ;
#11281=DIRECTION ( 'NONE',  ( 1.000000000000000000, -0.000000000000000000, -0.000000000000000000 ) ) ;
#11291=DIRECTION ( 'NONE',  ( -1.000000000000000000, 0.000000000000000000, 0.000000000000000000 ) ) ;
#11305=DIRECTION ( 'NONE',  ( 0.000000000000000000, 6.829619984160658243E-15, -1.000000000000000000 ) ) ;
#11393=VERTEX_POINT ( 'NONE', #31047 ) ;
#11399=( GEOMETRIC_REPRESENTATION_CONTEXT ( 3 ) GLOBAL_UNCERTAINTY_ASSIGNED_CONTEXT ( ( #15737 ) ) GLOBAL_UNIT_ASSIGNED_CONTEXT ( ( #1126, #26195, #23112 ) ) REPRESENTATION_CONTEXT ( 'NONE', 'WORKASPACE' ) );
#11428=CIRCLE ( 'NONE', #27212, 0.08000000000000000167 ) ;
#11430=CARTESIAN_POINT ( 'NONE',  ( -0.05464101615137770263, -2.116970787486931460, -0.3045972195783253067 ) ) ;
#11436=DIRECTION ( 'NONE',  ( -1.000000000000000000, -0.000000000000000000, -0.000000000000000000 ) ) ;
#11449=ORIENTED_EDGE ( 'NONE', *, *, #10692, .T. ) ;
#11456=AXIS2_PLACEMENT_3D ( 'NONE', #23395, #20479, #32406 ) ;
#11488=EDGE_CURVE ( 'NONE', #12909, #32770, #24475, .T. ) ;
#11505=DIRECTION ( 'NONE',  ( 1.000000000000000000, 0.000000000000000000, 0.000000000000000000 ) ) ;
#11515=FACE_OUTER_BOUND ( 'NONE', #30023, .T. ) ;
#11518=CARTESIAN_POINT ( 'NONE',  ( -0.02000000000000000042, -2.082394770077036661, -0.4779740388940064144 ) ) ;
#11542=ADVANCED_FACE ( 'NONE', ( #28961 ), #22410, .T. ) ;
#11567=FACE_OUTER_BOUND ( 'NONE', #8308, .T. ) ;
#11568=DIRECTION ( 'NONE',  ( 0.000000000000000000, 0.000000000000000000, 1.000000000000000000 ) ) ;
#11573=CARTESIAN_POINT ( 'NONE',  ( -0.02000000000000000042, -2.116970787486931460, -0.3045972195783253067 ) ) ;
#11600=CARTESIAN_POINT ( 'NONE',  ( -0.02000000000000000042, -2.183180860297908144, -0.4937760292030871079 ) ) ;
#11606=DIRECTION ( 'NONE',  ( -0.4999999999999969469, -0.5122356157878170668, -0.6982941170584776591 ) ) ;
#11646=ORIENTED_EDGE ( 'NONE', *, *, #22368, .F. ) ;
#11649=FACE_OUTER_BOUND ( 'NONE', #4815, .T. ) ;
#11657=DIRECTION ( 'NONE',  ( 1.000000000000000000, -0.000000000000000000, -0.000000000000000000 ) ) ;
#11664=EDGE_CURVE ( 'NONE', #29794, #30904, #16420, .T. ) ;
#11665=DIRECTION ( 'NONE',  ( -1.000000000000000000, -0.000000000000000000, -0.000000000000000000 ) ) ;
#11713=DIRECTION ( 'NONE',  ( 1.000000000000000000, 0.000000000000000000, 0.000000000000000000 ) ) ;
#11724=CARTESIAN_POINT ( 'NONE',  ( -0.02000000000000000042, -1.546789565643408526, -0.06332195561662121164 ) ) ;
#11773=EDGE_CURVE ( 'NONE', #12086, #14616, #35699, .T. ) ;
#11782=VERTEX_POINT ( 'NONE', #33061 ) ;
#11800=EDGE_CURVE ( 'NONE', #29395, #23547, #32853, .T. ) ;
#11814=CIRCLE ( 'NONE', #17166, 0.5088493849861025486 ) ;
#11819=ORIENTED_EDGE ( 'NONE', *, *, #28653, .F. ) ;
#11827=ADVANCED_FACE ( 'NONE', ( #18248 ), #37173, .T. ) ;
#11846=CARTESIAN_POINT ( 'NONE',  ( -0.05464101615137785528, -2.180132361182266720, -0.6941833704005058170 ) ) ;
#11851=CARTESIAN_POINT ( 'NONE',  ( -0.08000000000000000167, -1.984114763688379579, -0.7731012124309359912 ) ) ;
#11882=CIRCLE ( 'NONE', #18463, 0.07999999999999996003 ) ;
#11897=CARTESIAN_POINT ( 'NONE',  ( -0.05464101615137796630, -2.070343076906777213, -0.2454056712452573896 ) ) ;
#11936=DIRECTION ( 'NONE',  ( 0.4999999999999953926, 0.8179688131725333378, 0.2844767489218082979 ) ) ;
#11952=CIRCLE ( 'NONE', #34944, 0.1400000000000005684 ) ;
#11956=FACE_OUTER_BOUND ( 'NONE', #24146, .T. ) ;
#11972=CIRCLE ( 'NONE', #36960, 0.08000000000000000167 ) ;
#12000=EDGE_CURVE ( 'NONE', #34243, #13895, #6082, .T. ) ;
#12011=EDGE_CURVE ( 'NONE', #12860, #29794, #23214, .T. ) ;
#12049=ORIENTED_EDGE ( 'NONE', *, *, #18204, .F. ) ;
#12064=CARTESIAN_POINT ( 'NONE',  ( -0.07999999999999998779, -1.706654027108509997, -0.06438491259384498955 ) ) ;
#12070=AXIS2_PLACEMENT_3D ( 'NONE', #6200, #32245, #18769 ) ;
#12086=VERTEX_POINT ( 'NONE', #37554 ) ;
#12116=CARTESIAN_POINT ( 'NONE',  ( -0.05464101615137773038, -1.599201040860868339, 0.1642182323853691728 ) ) ;
#12123=CIRCLE ( 'NONE', #14762, 0.08000000000000000167 ) ;
#12169=EDGE_CURVE ( 'NONE', #24718, #12256, #7438, .T. ) ;
#12179=AXIS2_PLACEMENT_3D ( 'NONE', #39466, #11291, #19950 ) ;
#12192=CARTESIAN_POINT ( 'NONE',  ( -0.02000000000000000042, -2.241214508571226283, -0.3173949748123141568 ) ) ;
#12228=EDGE_CURVE ( 'NONE', #18399, #31675, #22564, .T. ) ;
#12239=AXIS2_PLACEMENT_3D ( 'NONE', #36642, #36437, #33342 ) ;
#12244=FACE_OUTER_BOUND ( 'NONE', #6589, .T. ) ;
#12256=VERTEX_POINT ( 'NONE', #30140 ) ;
#12260=CARTESIAN_POINT ( 'NONE',  ( -0.02000000000000000042, -2.177105168660885326, -0.2518349584362399862 ) ) ;
#12269=DIRECTION ( 'NONE',  ( 0.000000000000000000, 0.000000000000000000, -1.000000000000000000 ) ) ;
#12275=CIRCLE ( 'NONE', #35260, 0.08000000000000000167 ) ;
#12282=CARTESIAN_POINT ( 'NONE',  ( -0.02000000000000000042, -1.750394882718339762, -0.1142373872069606250 ) ) ;
#12302=VECTOR ( 'NONE', #37461, 39.37007874015748854 ) ;
#12339=ORIENTED_EDGE ( 'NONE', *, *, #21313, .T. ) ;
#12341=ORIENTED_EDGE ( 'NONE', *, *, #26320, .F. ) ;
#12343=DIRECTION ( 'NONE',  ( 0.000000000000000000, 0.000000000000000000, -1.000000000000000000 ) ) ;
#12348=DIRECTION ( 'NONE',  ( 0.000000000000000000, 0.000000000000000000, 1.000000000000000000 ) ) ;
#12353=DIRECTION ( 'NONE',  ( 1.000000000000000000, 0.000000000000000000, 0.000000000000000000 ) ) ;
#12381=ORIENTED_EDGE ( 'NONE', *, *, #33838, .F. ) ;
#12468=CARTESIAN_POINT ( 'NONE',  ( -0.02000000000000000042, -2.626773565144302935, -0.2726934094652516127 ) ) ;
#12469=EDGE_LOOP ( 'NONE', ( #20554, #8857 ) ) ;
#12476=LINE ( 'NONE', #21753, #15178 ) ;
#12482=DIRECTION ( 'NONE',  ( 0.3981087504120406351, -0.9173382270707808317, 0.000000000000000000 ) ) ;
#12543=VERTEX_POINT ( 'NONE', #15260 ) ;
#12549=ORIENTED_EDGE ( 'NONE', *, *, #38433, .T. ) ;
#12554=CARTESIAN_POINT ( 'NONE',  ( -0.02000000000000000042, -2.626773565144302935, -0.2526934094652523721 ) ) ;
#12560=DIRECTION ( 'NONE',  ( 0.4999999999999963918, -0.6509737717187614736, 0.5711682313769329555 ) ) ;
#12576=CARTESIAN_POINT ( 'NONE',  ( -0.05464101615137786222, -2.196538720661423749, -0.6552417777791260667 ) ) ;
#12578=CARTESIAN_POINT ( 'NONE',  ( -0.07999999999999998779, -2.180132361182266720, -0.6941833704005058170 ) ) ;
#12615=VECTOR ( 'NONE', #7724, 39.37007874015748854 ) ;
#12625=ORIENTED_EDGE ( 'NONE', *, *, #38566, .T. ) ;
#12639=CARTESIAN_POINT ( 'NONE',  ( -0.07999999999999998779, -2.367354784411275670, -0.3586747285825516718 ) ) ;
#12662=CARTESIAN_POINT ( 'NONE',  ( -0.02000000000000000042, -2.626773565144302935, -0.2726934094652516127 ) ) ;
#12668=CONICAL_SURFACE ( 'NONE', #5406, 0.1400000000000010403, 1.047197551196600962 ) ;
#12674=ADVANCED_FACE ( 'NONE', ( #32457 ), #38336, .F. ) ;
#12677=ADVANCED_FACE ( 'NONE', ( #3127 ), #29181, .F. ) ;
#12678=LINE ( 'NONE', #13503, #34431 ) ;
#12680=CIRCLE ( 'NONE', #35686, 0.7043128707267513056 ) ;
#12689=CYLINDRICAL_SURFACE ( 'NONE', #8265, 0.4488493849861021623 ) ;
#12693=DIRECTION ( 'NONE',  ( -1.000000000000000000, -0.000000000000000000, -0.000000000000000000 ) ) ;
#12712=DIRECTION ( 'NONE',  ( 0.000000000000000000, 6.829619984160658243E-15, -1.000000000000000000 ) ) ;
#12716=EDGE_CURVE ( 'NONE', #31436, #10881, #2243, .T. ) ;
#12717=VECTOR ( 'NONE', #5931, 39.37007874015748143 ) ;
#12733=AXIS2_PLACEMENT_3D ( 'NONE', #20345, #33680, #5490 ) ;
#12737=EDGE_CURVE ( 'NONE', #33509, #5941, #39644, .T. ) ;
#12741=VECTOR ( 'NONE', #30404, 39.37007874015748143 ) ;
#12752=ORIENTED_EDGE ( 'NONE', *, *, #2958, .T. ) ;
#12754=ADVANCED_FACE ( 'NONE', ( #10658 ), #1628, .T. ) ;
#12770=AXIS2_PLACEMENT_3D ( 'NONE', #27833, #21261, #24341 ) ;
#12774=LINE ( 'NONE', #34769, #18580 ) ;
#12782=CARTESIAN_POINT ( 'NONE',  ( -0.02000000000000000042, -1.712002775963388235, -0.1631032362481502906 ) ) ;
#12787=ADVANCED_FACE ( 'NONE', ( #17642 ), #17323, .F. ) ;
#12791=ORIENTED_EDGE ( 'NONE', *, *, #35182, .F. ) ;
#12812=CARTESIAN_POINT ( 'NONE',  ( -0.02000000000000000042, -1.727585455013649351, 0.002733164971117934498 ) ) ;
#12821=ORIENTED_EDGE ( 'NONE', *, *, #28653, .T. ) ;
#12830=CIRCLE ( 'NONE', #22046, 0.07999999999999996003 ) ;
#12841=ORIENTED_EDGE ( 'NONE', *, *, #20060, .T. ) ;
#12851=CARTESIAN_POINT ( 'NONE',  ( -0.02000000000000000042, -1.598492537578166672, -0.1971380022280825872 ) ) ;
#12855=VECTOR ( 'NONE', #13301, 39.37007874015748854 ) ;
#12860=VERTEX_POINT ( 'NONE', #39858 ) ;
#12883=DIRECTION ( 'NONE',  ( -1.000000000000000000, -0.000000000000000000, -0.000000000000000000 ) ) ;
#12903=CARTESIAN_POINT ( 'NONE',  ( -0.08000000000000000167, -2.039246558356380135, -0.5681570558249129377 ) ) ;
#12907=DIRECTION ( 'NONE',  ( 0.4999999999999981681, 0.7918451760093985214, 0.3506867793781887621 ) ) ;
#12909=VERTEX_POINT ( 'NONE', #40250 ) ;
#12935=EDGE_CURVE ( 'NONE', #10115, #17094, #40337, .T. ) ;
#12953=CARTESIAN_POINT ( 'NONE',  ( -0.02000000000000000042, -1.669835911085076674, -0.2333336242928227000 ) ) ;
#12966=ORIENTED_EDGE ( 'NONE', *, *, #23876, .T. ) ;
#12973=VERTEX_POINT ( 'NONE', #16581 ) ;
#12984=EDGE_CURVE ( 'NONE', #29116, #25808, #12678, .T. ) ;
#13017=CIRCLE ( 'NONE', #40603, 0.1620173459747806799 ) ;
#13021=DIRECTION ( 'NONE',  ( 0.000000000000000000, 0.000000000000000000, -1.000000000000000000 ) ) ;
#13044=CARTESIAN_POINT ( 'NONE',  ( -0.05464101615137768181, -2.367354784411275670, -0.3586747285825516718 ) ) ;
#13049=ORIENTED_EDGE ( 'NONE', *, *, #23072, .F. ) ;
#13053=DIRECTION ( 'NONE',  ( 1.000000000000000000, -0.000000000000000000, -0.000000000000000000 ) ) ;
#13057=VERTEX_POINT ( 'NONE', #4017 ) ;
#13077=DIRECTION ( 'NONE',  ( 0.000000000000000000, 1.951319995474463078E-15, -1.000000000000000000 ) ) ;
#13091=LINE ( 'NONE', #38381, #12615 ) ;
#13101=ORIENTED_EDGE ( 'NONE', *, *, #28599, .F. ) ;
#13105=DIRECTION ( 'NONE',  ( -1.000000000000000000, -0.000000000000000000, -0.000000000000000000 ) ) ;
#13154=DIRECTION ( 'NONE',  ( 0.000000000000000000, 0.000000000000000000, -1.000000000000000000 ) ) ;
#13157=DIRECTION ( 'NONE',  ( 0.4999999999999991118, -0.6509737717187596973, 0.5711682313769322894 ) ) ;
#13186=EDGE_CURVE ( 'NONE', #9415, #5797, #13412, .T. ) ;
#13233=DIRECTION ( 'NONE',  ( 0.000000000000000000, 0.000000000000000000, -1.000000000000000000 ) ) ;
#13301=DIRECTION ( 'NONE',  ( 0.4999999999999971134, 0.000000000000000000, -0.8660254037844402619 ) ) ;
#13327=CIRCLE ( 'NONE', #255, 0.07999999999999996003 ) ;
#13331=AXIS2_PLACEMENT_3D ( 'NONE', #11600, #20445, #33584 ) ;
#13343=EDGE_LOOP ( 'NONE', ( #746, #900, #29915, #4665, #32067 ) ) ;
#13344=ORIENTED_EDGE ( 'NONE', *, *, #387, .F. ) ;
#13355=ORIENTED_EDGE ( 'NONE', *, *, #16039, .T. ) ;
#13361=DIRECTION ( 'NONE',  ( 0.000000000000000000, 0.000000000000000000, -1.000000000000000000 ) ) ;
#13386=PRODUCT ( 'Outer shift plate', 'Outer shift plate', '', ( #17126 ) ) ;
#13387=DIRECTION ( 'NONE',  ( 1.000000000000000000, 0.000000000000000000, 0.000000000000000000 ) ) ;
#13396=ORIENTED_EDGE ( 'NONE', *, *, #20966, .F. ) ;
#13412=CIRCLE ( 'NONE', #11456, 0.1400000000000013456 ) ;
#13416=ORIENTED_EDGE ( 'NONE', *, *, #31898, .F. ) ;
#13419=DIRECTION ( 'NONE',  ( -0.4999999999999971134, 0.000000000000000000, 0.8660254037844402619 ) ) ;
#13433=EDGE_CURVE ( 'NONE', #19821, #5177, #37728, .T. ) ;
#13458=VERTEX_POINT ( 'NONE', #19626 ) ;
#13459=CYLINDRICAL_SURFACE ( 'NONE', #17234, 0.08000000000000000167 ) ;
#13463=CARTESIAN_POINT ( 'NONE',  ( -0.02000000000000000042, -2.177105168660885326, -0.2518349584362399862 ) ) ;
#13503=CARTESIAN_POINT ( 'NONE',  ( -0.02000000000000000042, -2.585754275622221154, -0.2040099479399058724 ) ) ;
#13506=ORIENTED_EDGE ( 'NONE', *, *, #31764, .T. ) ;
#13518=AXIS2_PLACEMENT_3D ( 'NONE', #8411, #5303, #3073 ) ;
#13627=CARTESIAN_POINT ( 'NONE',  ( -0.02000000000000000042, -1.622350287959229087, -0.08960079202753243321 ) ) ;
#13646=ORIENTED_EDGE ( 'NONE', *, *, #25007, .T. ) ;
#13648=FACE_OUTER_BOUND ( 'NONE', #28561, .T. ) ;
#13655=EDGE_CURVE ( 'NONE', #1334, #15898, #36189, .T. ) ;
#13683=ORIENTED_EDGE ( 'NONE', *, *, #14696, .F. ) ;
#13697=CARTESIAN_POINT ( 'NONE',  ( -0.02000000000000000042, -2.320036485105098301, -0.2941690811493925528 ) ) ;
#13764=DIRECTION ( 'NONE',  ( 0.000000000000000000, 0.000000000000000000, 1.000000000000000000 ) ) ;
#13765=EDGE_CURVE ( 'NONE', #19084, #33509, #1863, .T. ) ;
#13768=EDGE_CURVE ( 'NONE', #13895, #27138, #6846, .T. ) ;
#13781=CARTESIAN_POINT ( 'NONE',  ( -0.08000000000000000167, -2.631664041040912227, -0.5119035495255163104 ) ) ;
#13791=DIRECTION ( 'NONE',  ( 0.000000000000000000, 1.951319995474463472E-15, -1.000000000000000000 ) ) ;
#13793=EDGE_CURVE ( 'NONE', #13990, #1334, #37760, .T. ) ;
#13817=DIRECTION ( 'NONE',  ( -1.000000000000000000, -0.000000000000000000, -0.000000000000000000 ) ) ;
#13819=DIRECTION ( 'NONE',  ( 0.000000000000000000, 1.951319995474468994E-15, -1.000000000000000000 ) ) ;
#13822=DIRECTION ( 'NONE',  ( 0.000000000000000000, 0.8585432690668223232, -0.5127411190260187102 ) ) ;
#13838=ORIENTED_EDGE ( 'NONE', *, *, #32150, .T. ) ;
#13852=CARTESIAN_POINT ( 'NONE',  ( -0.02000000000000000042, -2.468922287121626091, -0.3957877349972418468 ) ) ;
#13868=DIRECTION ( 'NONE',  ( 0.000000000000000000, 0.000000000000000000, -1.000000000000000000 ) ) ;
#13894=CYLINDRICAL_SURFACE ( 'NONE', #9285, 0.08000000000000000167 ) ;
#13895=VERTEX_POINT ( 'NONE', #28164 ) ;
#13950=ORIENTED_EDGE ( 'NONE', *, *, #32147, .F. ) ;
#13953=ORIENTED_EDGE ( 'NONE', *, *, #30108, .T. ) ;
#13962=CARTESIAN_POINT ( 'NONE',  ( -0.05464101615137770263, -2.183180860297908144, -0.4937760292030871079 ) ) ;
#13990=VERTEX_POINT ( 'NONE', #15761 ) ;
#14001=VECTOR ( 'NONE', #8053, 39.37007874015748143 ) ;
#14004=VERTEX_POINT ( 'NONE', #30796 ) ;
#14025=DIRECTION ( 'NONE',  ( 0.000000000000000000, 0.000000000000000000, 1.000000000000000000 ) ) ;
#14054=ORIENTED_EDGE ( 'NONE', *, *, #14934, .F. ) ;
#14055=ORIENTED_EDGE ( 'NONE', *, *, #10577, .T. ) ;
#14059=AXIS2_PLACEMENT_3D ( 'NONE', #3276, #24291, #16644 ) ;
#14079=CIRCLE ( 'NONE', #18015, 0.5756329413417605734 ) ;
#14113=AXIS2_PLACEMENT_3D ( 'NONE', #8916, #2146, #2746 ) ;
#14116=CIRCLE ( 'NONE', #32522, 0.07999999999999996003 ) ;
#14149=DIRECTION ( 'NONE',  ( 1.000000000000000000, -0.000000000000000000, -0.000000000000000000 ) ) ;
#14190=DIRECTION ( 'NONE',  ( -1.000000000000000000, -0.000000000000000000, -0.000000000000000000 ) ) ;
#14209=VERTEX_POINT ( 'NONE', #23173 ) ;
#14223=ORIENTED_EDGE ( 'NONE', *, *, #11800, .T. ) ;
#14239=EDGE_CURVE ( 'NONE', #18110, #2068, #17408, .T. ) ;
#14256=ORIENTED_EDGE ( 'NONE', *, *, #26242, .T. ) ;
#14260=ORIENTED_EDGE ( 'NONE', *, *, #12716, .T. ) ;
#14278=EDGE_CURVE ( 'NONE', #39344, #25764, #6901, .T. ) ;
#14279=ORIENTED_EDGE ( 'NONE', *, *, #11773, .F. ) ;
#14280=DIRECTION ( 'NONE',  ( 0.000000000000000000, 0.000000000000000000, 1.000000000000000000 ) ) ;
#14293=LINE ( 'NONE', #33218, #28643 ) ;
#14294=CARTESIAN_POINT ( 'NONE',  ( -0.08000000000000000167, -1.968175500587574067, -0.6048844944454191408 ) ) ;
#14296=EDGE_LOOP ( 'NONE', ( #34641, #34802, #10428, #33912 ) ) ;
#14313=FACE_OUTER_BOUND ( 'NONE', #30419, .T. ) ;
#14315=ORIENTED_EDGE ( 'NONE', *, *, #1200, .F. ) ;
#14377=CARTESIAN_POINT ( 'NONE',  ( -0.08000000000000000167, -1.599201040860868339, 0.1642182323853691728 ) ) ;
#14389=ORIENTED_EDGE ( 'NONE', *, *, #31027, .T. ) ;
#14408=DIRECTION ( 'NONE',  ( -1.000000000000000000, -0.000000000000000000, -0.000000000000000000 ) ) ;
#14409=ORIENTED_EDGE ( 'NONE', *, *, #18042, .T. ) ;
#14426=EDGE_CURVE ( 'NONE', #26509, #29116, #30338, .T. ) ;
#14443=ORIENTED_EDGE ( 'NONE', *, *, #2898, .T. ) ;
#14446=ORIENTED_EDGE ( 'NONE', *, *, #16968, .T. ) ;
#14450=DIRECTION ( 'NONE',  ( -1.000000000000000000, -0.000000000000000000, -0.000000000000000000 ) ) ;
#14454=LINE ( 'NONE', #27023, #9294 ) ;
#14465=ORIENTED_EDGE ( 'NONE', *, *, #38413, .F. ) ;
#14520=EDGE_LOOP ( 'NONE', ( #19738, #3660, #22933, #37892, #35814, #1485, #6547, #19289, #8592 ) ) ;
#14556=ORIENTED_EDGE ( 'NONE', *, *, #19142, .F. ) ;
#14561=ORIENTED_EDGE ( 'NONE', *, *, #14934, .T. ) ;
#14578=CIRCLE ( 'NONE', #37567, 0.07999999999999996003 ) ;
#14589=CYLINDRICAL_SURFACE ( 'NONE', #4118, 0.08000000000000000167 ) ;
#14616=VERTEX_POINT ( 'NONE', #26017 ) ;
#14617=ORIENTED_EDGE ( 'NONE', *, *, #32150, .F. ) ;
#14623=CIRCLE ( 'NONE', #35652, 0.06250000000000001388 ) ;
#14624=DIRECTION ( 'NONE',  ( -1.000000000000000000, -0.000000000000000000, -0.000000000000000000 ) ) ;
#14642=AXIS2_PLACEMENT_3D ( 'NONE', #7393, #13387, #32109 ) ;
#14643=CYLINDRICAL_SURFACE ( 'NONE', #16885, 0.08000000000000002942 ) ;
#14646=AXIS2_PLACEMENT_3D ( 'NONE', #26049, #38568, #10197 ) ;
#14654=EDGE_LOOP ( 'NONE', ( #32860, #27774, #33295, #17643 ) ) ;
#14673=AXIS2_PLACEMENT_3D ( 'NONE', #18252, #21358, #33465 ) ;
#14696=EDGE_CURVE ( 'NONE', #16266, #5057, #14116, .T. ) ;
#14751=LINE ( 'NONE', #27096, #39788 ) ;
#14762=AXIS2_PLACEMENT_3D ( 'NONE', #519, #6413, #22481 ) ;
#14775=FACE_OUTER_BOUND ( 'NONE', #655, .T. ) ;
#14793=DIRECTION ( 'NONE',  ( -1.000000000000000000, -0.000000000000000000, -0.000000000000000000 ) ) ;
#14837=DIRECTION ( 'NONE',  ( 0.4999999999999967248, 0.4897188143951006767, -0.7142656948415344598 ) ) ;
#14867=VERTEX_POINT ( 'NONE', #39953 ) ;
#14875=ORIENTED_EDGE ( 'NONE', *, *, #38667, .T. ) ;
#14882=ORIENTED_EDGE ( 'NONE', *, *, #11247, .F. ) ;
#14908=EDGE_CURVE ( 'NONE', #29794, #24718, #1402, .T. ) ;
#14928=VERTEX_POINT ( 'NONE', #5990 ) ;
#14930=CARTESIAN_POINT ( 'NONE',  ( -0.05464101615137786222, -2.321277022828569958, -0.5785054236952983375 ) ) ;
#14932=LINE ( 'NONE', #33635, #25971 ) ;
#14934=EDGE_CURVE ( 'NONE', #14004, #14616, #5592, .T. ) ;
#14957=FACE_BOUND ( 'NONE', #20264, .T. ) ;
#14964=EDGE_CURVE ( 'NONE', #18164, #38792, #21250, .T. ) ;
#15020=EDGE_CURVE ( 'NONE', #2801, #10878, #19171, .T. ) ;
#15021=DIRECTION ( 'NONE',  ( -1.000000000000000000, -0.000000000000000000, -0.000000000000000000 ) ) ;
#15039=DIRECTION ( 'NONE',  ( 0.000000000000000000, 0.000000000000000000, 1.000000000000000000 ) ) ;
#15064=EDGE_LOOP ( 'NONE', ( #30669, #27576, #17655, #39916 ) ) ;
#15071=ORIENTED_EDGE ( 'NONE', *, *, #2043, .T. ) ;
#15085=ORIENTED_EDGE ( 'NONE', *, *, #10405, .F. ) ;
#15114=LINE ( 'NONE', #18404, #34471 ) ;
#15128=ORIENTED_EDGE ( 'NONE', *, *, #8220, .T. ) ;
#15135=DIRECTION ( 'NONE',  ( 0.000000000000000000, 0.8585432690668223232, -0.5127411190260187102 ) ) ;
#15171=ORIENTED_EDGE ( 'NONE', *, *, #23355, .T. ) ;
#15178=VECTOR ( 'NONE', #34284, 39.37007874015748854 ) ;
#15184=ORIENTED_EDGE ( 'NONE', *, *, #7367, .T. ) ;
#15214=ORIENTED_EDGE ( 'NONE', *, *, #5982, .T. ) ;
#15232=ORIENTED_EDGE ( 'NONE', *, *, #10452, .F. ) ;
#15234=CARTESIAN_POINT ( 'NONE',  ( -0.08000000000000000167, -2.230494317742474308, -0.6487310457122437146 ) ) ;
#15238=VECTOR ( 'NONE', #14837, 39.37007874015748854 ) ;
#15242=CIRCLE ( 'NONE', #7971, 0.08000000000000002942 ) ;
#15251=FACE_OUTER_BOUND ( 'NONE', #28224, .T. ) ;
#15260=CARTESIAN_POINT ( 'NONE',  ( -0.02000000000000000042, -2.579110126769056599, -0.2778638008585438413 ) ) ;
#15277=DIRECTION ( 'NONE',  ( 1.000000000000000000, -0.000000000000000000, -0.000000000000000000 ) ) ;
#15281=EDGE_LOOP ( 'NONE', ( #20747, #34104, #209, #26567 ) ) ;
#15335=EDGE_LOOP ( 'NONE', ( #6461, #21107, #31465, #30764, #23741 ) ) ;
#15343=EDGE_CURVE ( 'NONE', #6598, #17659, #12476, .T. ) ;
#15387=ORIENTED_EDGE ( 'NONE', *, *, #30387, .T. ) ;
#15399=FACE_OUTER_BOUND ( 'NONE', #17249, .T. ) ;
#15403=DIRECTION ( 'NONE',  ( 0.000000000000000000, 0.000000000000000000, -1.000000000000000000 ) ) ;
#15419=DIRECTION ( 'NONE',  ( 1.000000000000000000, 0.000000000000000000, 0.000000000000000000 ) ) ;
#15428=DIRECTION ( 'NONE',  ( 1.000000000000000000, 0.000000000000000000, 0.000000000000000000 ) ) ;
#15472=VECTOR ( 'NONE', #26148, 39.37007874015748143 ) ;
#15473=CARTESIAN_POINT ( 'NONE',  ( -0.08000000000000000167, -2.183180860297908144, -0.4937760292030871079 ) ) ;
#15477=EDGE_CURVE ( 'NONE', #29445, #8808, #13091, .T. ) ;
#15479=VERTEX_POINT ( 'NONE', #2174 ) ;
#15509=AXIS2_PLACEMENT_3D ( 'NONE', #17328, #1315, #13822 ) ;
#15534=ORIENTED_EDGE ( 'NONE', *, *, #32123, .F. ) ;
#15540=DIRECTION ( 'NONE',  ( 0.000000000000000000, 0.000000000000000000, 1.000000000000000000 ) ) ;
#15562=DIRECTION ( 'NONE',  ( 0.000000000000000000, 0.6595282642760668113, 0.7516797646744247663 ) ) ;
#15574=VECTOR ( 'NONE', #27083, 39.37007874015748143 ) ;
#15605=ORIENTED_EDGE ( 'NONE', *, *, #32047, .T. ) ;
#15608=ORIENTED_EDGE ( 'NONE', *, *, #26845, .F. ) ;
#15627=CIRCLE ( 'NONE', #28757, 0.08000000000000002942 ) ;
#15648=CARTESIAN_POINT ( 'NONE',  ( -0.02000000000000000042, -2.124839267114085217, -0.6708880114557002061 ) ) ;
#15660=DIRECTION ( 'NONE',  ( 0.000000000000000000, 0.6595282642760672553, 0.7516797646744243222 ) ) ;
#15674=VERTEX_POINT ( 'NONE', #28472 ) ;
#15683=DIRECTION ( 'NONE',  ( 1.000000000000000000, -0.000000000000000000, -0.000000000000000000 ) ) ;
#15691=ORIENTED_EDGE ( 'NONE', *, *, #10399, .F. ) ;
#15699=EDGE_CURVE ( 'NONE', #2068, #16485, #21181, .T. ) ;
#15737=UNCERTAINTY_MEASURE_WITH_UNIT (LENGTH_MEASURE( 1.000000000000000082E-05 ), #1126, 'distance_accuracy_value', 'NONE');
#15761=CARTESIAN_POINT ( 'NONE',  ( -0.08000000000000000167, -2.004218822785767795, -0.4035264592197354561 ) ) ;
#15763=EDGE_CURVE ( 'NONE', #2769, #30547, #35265, .T. ) ;
#15799=DIRECTION ( 'NONE',  ( -1.000000000000000000, 0.000000000000000000, 0.000000000000000000 ) ) ;
#15804=ADVANCED_FACE ( 'NONE', ( #37942 ), #23158, .T. ) ;
#15822=ORIENTED_EDGE ( 'NONE', *, *, #19187, .F. ) ;
#15835=ORIENTED_EDGE ( 'NONE', *, *, #23255, .T. ) ;
#15839=DIRECTION ( 'NONE',  ( 1.000000000000000000, -0.000000000000000000, -0.000000000000000000 ) ) ;
#15862=VECTOR ( 'NONE', #21038, 39.37007874015748143 ) ;
#15879=ADVANCED_FACE ( 'NONE', ( #6650 ), #13459, .T. ) ;
#15896=DIRECTION ( 'NONE',  ( -1.000000000000000000, -0.000000000000000000, -0.000000000000000000 ) ) ;
#15898=VERTEX_POINT ( 'NONE', #22323 ) ;
#15910=CIRCLE ( 'NONE', #24465, 0.1400000000000007350 ) ;
#15916=VERTEX_POINT ( 'NONE', #34839 ) ;
#15924=ORIENTED_EDGE ( 'NONE', *, *, #38545, .F. ) ;
#15929=ADVANCED_FACE ( 'NONE', ( #13648 ), #25771, .T. ) ;
#15942=DIRECTION ( 'NONE',  ( -1.000000000000000000, -0.000000000000000000, -0.000000000000000000 ) ) ;
#15947=DIRECTION ( 'NONE',  ( 0.000000000000000000, -0.3882559824134205195, 0.9215515678030119506 ) ) ;
#15972=VECTOR ( 'NONE', #8012, 39.37007874015748143 ) ;
#15980=CIRCLE ( 'NONE', #35773, 0.07999999999999996003 ) ;
#15981=ORIENTED_EDGE ( 'NONE', *, *, #24647, .F. ) ;
#16003=ORIENTED_EDGE ( 'NONE', *, *, #12737, .T. ) ;
#16005=EDGE_LOOP ( 'NONE', ( #2717, #14409, #19677, #22844 ) ) ;
#16012=VECTOR ( 'NONE', #38826, 39.37007874015748854 ) ;
#16015=DIRECTION ( 'NONE',  ( 0.000000000000000000, 0.000000000000000000, 1.000000000000000000 ) ) ;
#16017=CARTESIAN_POINT ( 'NONE',  ( -0.02000000000000000042, -1.968175500587574067, -0.6048844944454191408 ) ) ;
#16033=AXIS2_PLACEMENT_3D ( 'NONE', #17192, #11220, #1795 ) ;
#16035=FACE_OUTER_BOUND ( 'NONE', #17144, .T. ) ;
#16038=ORIENTED_EDGE ( 'NONE', *, *, #38413, .T. ) ;
#16039=EDGE_CURVE ( 'NONE', #17786, #1840, #37572, .T. ) ;
#16044=FACE_OUTER_BOUND ( 'NONE', #35723, .T. ) ;
#16049=VECTOR ( 'NONE', #9772, 39.37007874015748143 ) ;
#16057=EDGE_CURVE ( 'NONE', #6598, #37905, #37608, .T. ) ;
#16075=FACE_OUTER_BOUND ( 'NONE', #33847, .T. ) ;
#16082=CARTESIAN_POINT ( 'NONE',  ( -0.05464101615137768181, -1.699711333021935777, -0.9366211149475224262 ) ) ;
#16088=CARTESIAN_POINT ( 'NONE',  ( -0.02000000000000000042, -2.097192720079996242, -0.6592403319832980113 ) ) ;
#16099=DIRECTION ( 'NONE',  ( 0.4999999999999966693, 0.7750948722061129503, -0.3863003223915205675 ) ) ;
#16107=VERTEX_POINT ( 'NONE', #29034 ) ;
#16108=VECTOR ( 'NONE', #38048, 39.37007874015748854 ) ;
#16115=VECTOR ( 'NONE', #7994, 39.37007874015748143 ) ;
#16141=EDGE_LOOP ( 'NONE', ( #38333, #9335, #2925, #24942 ) ) ;
#16176=AXIS2_PLACEMENT_3D ( 'NONE', #38364, #19259, #31803 ) ;
#16196=CIRCLE ( 'NONE', #37865, 0.1400000000000005684 ) ;
#16215=DIRECTION ( 'NONE',  ( 0.000000000000000000, -3.414809992080329122E-15, -1.000000000000000000 ) ) ;
#16236=CARTESIAN_POINT ( 'NONE',  ( -0.07999999999999998779, -2.504411011601259673, -0.4441669705721119632 ) ) ;
#16247=ORIENTED_EDGE ( 'NONE', *, *, #24087, .T. ) ;
#16250=VERTEX_POINT ( 'NONE', #18316 ) ;
#16252=CARTESIAN_POINT ( 'NONE',  ( -0.02000000000000000042, -2.071870001606465284, -0.3441689154348898105 ) ) ;
#16254=LINE ( 'NONE', #32076, #10101 ) ;
#16266=VERTEX_POINT ( 'NONE', #18725 ) ;
#16271=DIRECTION ( 'NONE',  ( 1.000000000000000000, -0.000000000000000000, -0.000000000000000000 ) ) ;
#16283=AXIS2_PLACEMENT_3D ( 'NONE', #29647, #35614, #26577 ) ;
#16290=CARTESIAN_POINT ( 'NONE',  ( -0.02000000000000000042, -2.183180860297908144, -0.4312760292030870524 ) ) ;
#16300=ADVANCED_FACE ( 'NONE', ( #5550 ), #8629, .T. ) ;
#16303=CARTESIAN_POINT ( 'NONE',  ( -0.05464101615137795936, -1.598492537578166672, -0.1971380022280825872 ) ) ;
#16304=EDGE_LOOP ( 'NONE', ( #19841, #14055, #26735, #9345, #14875, #7123, #6804, #15184, #28267, #3896, #30704, #8027, #5996, #6300, #40, #16980, #9965 ) ) ;
#16346=DIRECTION ( 'NONE',  ( 1.000000000000000000, 0.000000000000000000, 0.000000000000000000 ) ) ;
#16385=LINE ( 'NONE', #793, #12855 ) ;
#16420=LINE ( 'NONE', #31862, #2850 ) ;
#16425=CYLINDRICAL_SURFACE ( 'NONE', #38107, 0.07999999999999996003 ) ;
#16430=ORIENTED_EDGE ( 'NONE', *, *, #8675, .T. ) ;
#16440=ADVANCED_FACE ( 'NONE', ( #25512 ), #1060, .T. ) ;
#16484=EDGE_LOOP ( 'NONE', ( #28595, #11449, #37996, #21012 ) ) ;
#16485=VERTEX_POINT ( 'NONE', #19344 ) ;
#16487=DIRECTION ( 'NONE',  ( 0.000000000000000000, 0.000000000000000000, -1.000000000000000000 ) ) ;
#16522=CARTESIAN_POINT ( 'NONE',  ( -0.02000000000000000042, -2.548345659627495596, -0.2263512047145338768 ) ) ;
#16539=DIRECTION ( 'NONE',  ( 1.000000000000000000, 0.000000000000000000, 0.000000000000000000 ) ) ;
#16546=VECTOR ( 'NONE', #15947, 39.37007874015748854 ) ;
#16552=DIRECTION ( 'NONE',  ( 0.000000000000000000, -6.829619984160655877E-15, -1.000000000000000000 ) ) ;
#16564=FACE_OUTER_BOUND ( 'NONE', #22688, .T. ) ;
#16580=DIRECTION ( 'NONE',  ( -1.000000000000000000, -0.000000000000000000, -0.000000000000000000 ) ) ;
#16581=CARTESIAN_POINT ( 'NONE',  ( -0.05464101615137773038, -1.599201040860868339, 0.2442182323853691606 ) ) ;
#16610=CARTESIAN_POINT ( 'NONE',  ( -0.02000000000000000042, -1.723343441215260619, -0.2604803408413784993 ) ) ;
#16622=AXIS2_PLACEMENT_3D ( 'NONE', #7978, #11281, #23848 ) ;
#16634=DIRECTION ( 'NONE',  ( -1.000000000000000000, -0.000000000000000000, -0.000000000000000000 ) ) ;
#16644=DIRECTION ( 'NONE',  ( 0.000000000000000000, 0.000000000000000000, -1.000000000000000000 ) ) ;
#16652=AXIS2_PLACEMENT_3D ( 'NONE', #35357, #10871, #20335 ) ;
#16682=ADVANCED_FACE ( 'NONE', ( #36168 ), #30429, .F. ) ;
#16686=CIRCLE ( 'NONE', #31168, 0.06250000000000001388 ) ;
#16689=CYLINDRICAL_SURFACE ( 'NONE', #26951, 0.08000000000000002942 ) ;
#16708=VERTEX_POINT ( 'NONE', #6460 ) ;
#16757=DIRECTION ( 'NONE',  ( 0.000000000000000000, 0.000000000000000000, -1.000000000000000000 ) ) ;
#16768=VECTOR ( 'NONE', #38460, 39.37007874015748854 ) ;
#16785=DIRECTION ( 'NONE',  ( 1.000000000000000000, 0.000000000000000000, 0.000000000000000000 ) ) ;
#16814=ORIENTED_EDGE ( 'NONE', *, *, #7022, .T. ) ;
#16838=ADVANCED_FACE ( 'NONE', ( #32980 ), #39771, .T. ) ;
#16849=DIRECTION ( 'NONE',  ( -1.000000000000000000, -0.000000000000000000, -0.000000000000000000 ) ) ;
#16855=LINE ( 'NONE', #29398, #768 ) ;
#16861=AXIS2_PLACEMENT_3D ( 'NONE', #28602, #15839, #10294 ) ;
#16875=DIRECTION ( 'NONE',  ( -1.000000000000000000, -0.000000000000000000, -0.000000000000000000 ) ) ;
#16885=AXIS2_PLACEMENT_3D ( 'NONE', #39341, #11160, #1523 ) ;
#16909=CARTESIAN_POINT ( 'NONE',  ( -0.08000000000000000167, -2.332630956013932888, -0.5701767140373721343 ) ) ;
#16951=DIRECTION ( 'NONE',  ( 0.4999999999999972244, 0.000000000000000000, -0.8660254037844402619 ) ) ;
#16968=EDGE_CURVE ( 'NONE', #7866, #12909, #20183, .T. ) ;
#16980=ORIENTED_EDGE ( 'NONE', *, *, #17010, .T. ) ;
#16991=ORIENTED_EDGE ( 'NONE', *, *, #769, .F. ) ;
#17010=EDGE_CURVE ( 'NONE', #34558, #38795, #23865, .T. ) ;
#17015=ORIENTED_EDGE ( 'NONE', *, *, #21052, .F. ) ;
#17085=VECTOR ( 'NONE', #18101, 39.37007874015748143 ) ;
#17094=VERTEX_POINT ( 'NONE', #13781 ) ;
#17126=PRODUCT_CONTEXT ( 'NONE', #5310, 'mechanical' ) ;
#17129=FACE_OUTER_BOUND ( 'NONE', #26170, .T. ) ;
#17134=AXIS2_PLACEMENT_3D ( 'NONE', #17563, #36481, #30106 ) ;
#17144=EDGE_LOOP ( 'NONE', ( #38774, #3359, #5952, #7481, #2637 ) ) ;
#17147=FACE_OUTER_BOUND ( 'NONE', #27950, .T. ) ;
#17148=AXIS2_PLACEMENT_3D ( 'NONE', #12260, #34053, #27490 ) ;
#17161=DIRECTION ( 'NONE',  ( 1.000000000000000000, -0.000000000000000000, -0.000000000000000000 ) ) ;
#17166=AXIS2_PLACEMENT_3D ( 'NONE', #8814, #14793, #18079 ) ;
#17192=CARTESIAN_POINT ( 'NONE',  ( -0.02000000000000000042, -1.646519645934556131, -0.1171471737359304072 ) ) ;
#17199=CARTESIAN_POINT ( 'NONE',  ( -0.08000000000000000167, -2.504411011601259673, -0.4441669705721119632 ) ) ;
#17230=CIRCLE ( 'NONE', #189, 0.08000000000000002942 ) ;
#17231=VECTOR ( 'NONE', #31910, 39.37007874015748143 ) ;
#17234=AXIS2_PLACEMENT_3D ( 'NONE', #26025, #22934, #3789 ) ;
#17249=EDGE_LOOP ( 'NONE', ( #25565, #5707, #39158, #13344 ) ) ;
#17258=DIRECTION ( 'NONE',  ( 0.000000000000000000, 0.000000000000000000, 1.000000000000000000 ) ) ;
#17259=AXIS2_PLACEMENT_3D ( 'NONE', #21225, #33763, #30260 ) ;
#17263=DIRECTION ( 'NONE',  ( 0.000000000000000000, 0.000000000000000000, 1.000000000000000000 ) ) ;
#17265=AXIS2_PLACEMENT_3D ( 'NONE', #36403, #8008, #8416 ) ;
#17269=AXIS2_PLACEMENT_3D ( 'NONE', #40528, #5758, #12348 ) ;
#17301=EDGE_CURVE ( 'NONE', #37987, #15898, #34771, .T. ) ;
#17323=CONICAL_SURFACE ( 'NONE', #311, 0.1400000000000009570, 1.047197551196600962 ) ;
#17328=CARTESIAN_POINT ( 'NONE',  ( -0.02000000000000000042, -2.545097362529205487, -0.2282911599260125379 ) ) ;
#17334=AXIS2_PLACEMENT_3D ( 'NONE', #13627, #38716, #10748 ) ;
#17365=AXIS2_PLACEMENT_3D ( 'NONE', #39280, #30032, #4317 ) ;
#17385=CARTESIAN_POINT ( 'NONE',  ( -0.05464101615137786222, -2.332630956013932888, -0.5701767140373721343 ) ) ;
#17386=CARTESIAN_POINT ( 'NONE',  ( -0.08000000000000000167, -2.313818782766725146, -0.3979462133327477114 ) ) ;
#17408=CIRCLE ( 'NONE', #19395, 0.5543128707267515054 ) ;
#17438=DIRECTION ( 'NONE',  ( -1.000000000000000000, -0.000000000000000000, -0.000000000000000000 ) ) ;
#17473=LINE ( 'NONE', #33097, #15472 ) ;
#17486=CARTESIAN_POINT ( 'NONE',  ( -0.02000000000000000042, -2.281505296119629378, -0.5332679964655872018 ) ) ;
#17497=CARTESIAN_POINT ( 'NONE',  ( -0.02000000000000000042, -1.518907846805490403, -0.1889969338327479598 ) ) ;
#17518=ORIENTED_EDGE ( 'NONE', *, *, #2725, .T. ) ;
#17529=AXIS2_PLACEMENT_3D ( 'NONE', #12282, #175, #24839 ) ;
#17563=CARTESIAN_POINT ( 'NONE',  ( -0.08000000000000000167, -2.183180860297908144, -0.4937760292030871079 ) ) ;
#17598=CARTESIAN_POINT ( 'NONE',  ( -0.08000000000000000167, -2.545097362529205487, -0.2282911599260125379 ) ) ;
#17601=ORIENTED_EDGE ( 'NONE', *, *, #18841, .T. ) ;
#17618=ORIENTED_EDGE ( 'NONE', *, *, #32662, .F. ) ;
#17642=FACE_OUTER_BOUND ( 'NONE', #22632, .T. ) ;
#17643=ORIENTED_EDGE ( 'NONE', *, *, #25566, .F. ) ;
#17655=ORIENTED_EDGE ( 'NONE', *, *, #23252, .F. ) ;
#17659=VERTEX_POINT ( 'NONE', #27554 ) ;
#17664=DIRECTION ( 'NONE',  ( 0.4999999999999978351, 0.7980870686147867321, 0.3362395439413078391 ) ) ;
#17674=DIRECTION ( 'NONE',  ( -1.000000000000000000, -0.000000000000000000, -0.000000000000000000 ) ) ;
#17684=ORIENTED_EDGE ( 'NONE', *, *, #15477, .F. ) ;
#17708=EDGE_CURVE ( 'NONE', #19134, #34885, #6533, .T. ) ;
#17728=EDGE_CURVE ( 'NONE', #15674, #13990, #9831, .T. ) ;
#17766=DIRECTION ( 'NONE',  ( 0.000000000000000000, 0.6595282642760673664, 0.7516797646744242112 ) ) ;
#17782=AXIS2_PLACEMENT_3D ( 'NONE', #103, #15896, #13021 ) ;
#17786=VERTEX_POINT ( 'NONE', #9217 ) ;
#17794=CYLINDRICAL_SURFACE ( 'NONE', #34555, 0.07999999999999996003 ) ;
#17800=DIRECTION ( 'NONE',  ( 0.000000000000000000, 0.000000000000000000, -1.000000000000000000 ) ) ;
#17812=CARTESIAN_POINT ( 'NONE',  ( -0.08000000000000000167, -1.538828486247671101, 0.2167077994389899898 ) ) ;
#17835=DIRECTION ( 'NONE',  ( 0.8660254037844409281, -0.3758398823372091635, 0.3297641321380309631 ) ) ;
#17848=ORIENTED_EDGE ( 'NONE', *, *, #15020, .F. ) ;
#17861=DIRECTION ( 'NONE',  ( -0.4999999999999976685, 0.7693667687702180347, -0.3975861857661508458 ) ) ;
#17867=AXIS2_PLACEMENT_3D ( 'NONE', #36442, #30074, #18329 ) ;
#17870=CARTESIAN_POINT ( 'NONE',  ( -0.08000000000000000167, -2.183180860297908144, -0.4312760292030870524 ) ) ;
#17873=VECTOR ( 'NONE', #16539, 39.37007874015748143 ) ;
#17889=ORIENTED_EDGE ( 'NONE', *, *, #3735, .T. ) ;
#17898=CARTESIAN_POINT ( 'NONE',  ( -0.05464101615137769569, -1.758704040287260018, -0.8825853814972600686 ) ) ;
#17937=CARTESIAN_POINT ( 'NONE',  ( -0.08000000000000000167, -2.698373762442814350, -0.2370085142459261163 ) ) ;
#18015=AXIS2_PLACEMENT_3D ( 'NONE', #19227, #16346, #35269 ) ;
#18027=DIRECTION ( 'NONE',  ( 1.000000000000000000, 0.000000000000000000, 0.000000000000000000 ) ) ;
#18042=EDGE_CURVE ( 'NONE', #30547, #4481, #34319, .T. ) ;
#18062=ORIENTED_EDGE ( 'NONE', *, *, #2898, .F. ) ;
#18079=DIRECTION ( 'NONE',  ( 0.000000000000000000, -1.610603102373135995E-15, -1.000000000000000000 ) ) ;
#18101=DIRECTION ( 'NONE',  ( -1.000000000000000000, -0.000000000000000000, -0.000000000000000000 ) ) ;
#18103=ORIENTED_EDGE ( 'NONE', *, *, #31535, .T. ) ;
#18110=VERTEX_POINT ( 'NONE', #9273 ) ;
#18117=CYLINDRICAL_SURFACE ( 'NONE', #376, 0.08000000000000000167 ) ;
#18130=DIRECTION ( 'NONE',  ( 0.000000000000000000, 0.3882559824134196313, -0.9215515678030125057 ) ) ;
#18146=CARTESIAN_POINT ( 'NONE',  ( -0.05464101615137795936, -1.598492537578166672, -0.2771380022280826028 ) ) ;
#18155=ORIENTED_EDGE ( 'NONE', *, *, #27330, .F. ) ;
#18164=VERTEX_POINT ( 'NONE', #3304 ) ;
#18179=EDGE_CURVE ( 'NONE', #37196, #9415, #3118, .T. ) ;
#18204=EDGE_CURVE ( 'NONE', #7855, #31436, #9487, .T. ) ;
#18215=ORIENTED_EDGE ( 'NONE', *, *, #17708, .T. ) ;
#18248=FACE_OUTER_BOUND ( 'NONE', #40104, .T. ) ;
#18252=CARTESIAN_POINT ( 'NONE',  ( -0.05464101615137761936, -1.845925619402022155, -0.3444148183989317880 ) ) ;
#18260=DIRECTION ( 'NONE',  ( -1.000000000000000000, -0.000000000000000000, -0.000000000000000000 ) ) ;
#18292=CARTESIAN_POINT ( 'NONE',  ( -0.02000000000000000042, -2.691615088641019504, -0.5143267481657003426 ) ) ;
#18303=CARTESIAN_POINT ( 'NONE',  ( -0.02000000000000000042, -2.183180860297908144, -0.4937760292030871079 ) ) ;
#18307=ORIENTED_EDGE ( 'NONE', *, *, #20572, .T. ) ;
#18309=EDGE_LOOP ( 'NONE', ( #28928, #26522, #13101, #38678 ) ) ;
#18316=CARTESIAN_POINT ( 'NONE',  ( -0.02000000000000000042, -2.183180860297908144, -0.4312760292030870524 ) ) ;
#18329=DIRECTION ( 'NONE',  ( 0.000000000000000000, 0.000000000000000000, -1.000000000000000000 ) ) ;
#18331=EDGE_CURVE ( 'NONE', #5340, #9944, #11972, .T. ) ;
#18339=DIRECTION ( 'NONE',  ( 0.000000000000000000, -0.8063205929144886541, 0.5914787413272157846 ) ) ;
#18399=VERTEX_POINT ( 'NONE', #23878 ) ;
#18404=CARTESIAN_POINT ( 'NONE',  ( -0.05464101615137785528, -2.230494317742474308, -0.6487310457122437146 ) ) ;
#18429=AXIS2_PLACEMENT_3D ( 'NONE', #31058, #2878, #31274 ) ;
#18463=AXIS2_PLACEMENT_3D ( 'NONE', #32017, #787, #407 ) ;
#18571=DIRECTION ( 'NONE',  ( 0.000000000000000000, 0.000000000000000000, -1.000000000000000000 ) ) ;
#18580=VECTOR ( 'NONE', #12560, 39.37007874015747433 ) ;
#18590=EDGE_CURVE ( 'NONE', #17094, #21046, #36142, .T. ) ;
#18615=DIRECTION ( 'NONE',  ( -1.000000000000000000, -0.000000000000000000, -0.000000000000000000 ) ) ;
#18617=CARTESIAN_POINT ( 'NONE',  ( -0.02000000000000000042, -2.183180860297908144, -0.4937760292030871079 ) ) ;
#18637=DIRECTION ( 'NONE',  ( 0.000000000000000000, 0.000000000000000000, -1.000000000000000000 ) ) ;
#18644=VECTOR ( 'NONE', #33955, 39.37007874015747433 ) ;
#18649=CARTESIAN_POINT ( 'NONE',  ( -0.02000000000000000042, -1.490119023906541607, -0.04361282830843733055 ) ) ;
#18651=CIRCLE ( 'NONE', #30488, 0.5756329413417605734 ) ;
#18653=AXIS2_PLACEMENT_3D ( 'NONE', #1720, #1312, #13819 ) ;
#18667=ORIENTED_EDGE ( 'NONE', *, *, #18331, .T. ) ;
#18685=ORIENTED_EDGE ( 'NONE', *, *, #29485, .F. ) ;
#18725=CARTESIAN_POINT ( 'NONE',  ( -0.08000000000000000167, -1.737515812098395118, -0.8661170628529262228 ) ) ;
#18756=ADVANCED_FACE ( 'NONE', ( #14957, #36566, #26904, #8562, #39850 ), #24227, .T. ) ;
#18769=DIRECTION ( 'NONE',  ( 0.000000000000000000, 0.000000000000000000, -1.000000000000000000 ) ) ;
#18772=CARTESIAN_POINT ( 'NONE',  ( -0.02000000000000000042, -1.851224977018630868, -0.7958870385335592434 ) ) ;
#18777=ORIENTED_EDGE ( 'NONE', *, *, #14239, .T. ) ;
#18794=DIRECTION ( 'NONE',  ( -1.000000000000000000, -0.000000000000000000, -0.000000000000000000 ) ) ;
#18797=DIRECTION ( 'NONE',  ( 1.000000000000000000, 0.000000000000000000, 0.000000000000000000 ) ) ;
#18807=( NAMED_UNIT ( * ) SI_UNIT ( $, .STERADIAN. ) SOLID_ANGLE_UNIT ( ) );
#18841=EDGE_CURVE ( 'NONE', #7253, #13057, #13327, .T. ) ;
#18849=CARTESIAN_POINT ( 'NONE',  ( -0.05464101615137786222, -2.122347498858831116, -0.8313396097929491857 ) ) ;
#18865=CARTESIAN_POINT ( 'NONE',  ( -0.05464101615137769569, -2.179113517810423062, -0.3318097452986852880 ) ) ;
#18910=LINE ( 'NONE', #18292, #21887 ) ;
#18931=FACE_OUTER_BOUND ( 'NONE', #39585, .T. ) ;
#18937=DIRECTION ( 'NONE',  ( 0.8660254037844402619, 0.2957393706636063380, 0.4031602964572422731 ) ) ;
#18990=VERTEX_POINT ( 'NONE', #1362 ) ;
#19022=DIRECTION ( 'NONE',  ( 1.000000000000000000, 0.000000000000000000, 0.000000000000000000 ) ) ;
#19035=ORIENTED_EDGE ( 'NONE', *, *, #21741, .F. ) ;
#19036=CARTESIAN_POINT ( 'NONE',  ( -0.05464101615137795936, -1.712002775963388235, -0.1631032362481502906 ) ) ;
#19047=FACE_BOUND ( 'NONE', #27227, .T. ) ;
#19083=ORIENTED_EDGE ( 'NONE', *, *, #35356, .F. ) ;
#19084=VERTEX_POINT ( 'NONE', #7713 ) ;
#19100=DIRECTION ( 'NONE',  ( -1.000000000000000000, -0.000000000000000000, -0.000000000000000000 ) ) ;
#19129=DIRECTION ( 'NONE',  ( 1.000000000000000000, -0.000000000000000000, -0.000000000000000000 ) ) ;
#19134=VERTEX_POINT ( 'NONE', #29724 ) ;
#19142=EDGE_CURVE ( 'NONE', #8899, #22200, #5227, .T. ) ;
#19167=DIRECTION ( 'NONE',  ( -1.000000000000000000, -0.000000000000000000, -0.000000000000000000 ) ) ;
#19171=LINE ( 'NONE', #12578, #2055 ) ;
#19187=EDGE_CURVE ( 'NONE', #17094, #7319, #2176, .T. ) ;
#19192=CARTESIAN_POINT ( 'NONE',  ( -0.02000000000000000042, -2.196071624283071788, -0.8624000883860228894 ) ) ;
#19198=CARTESIAN_POINT ( 'NONE',  ( -0.02000000000000000042, -1.622350287959229087, -0.009600792027532436754 ) ) ;
#19227=CARTESIAN_POINT ( 'NONE',  ( -0.08000000000000000167, -2.183180860297908144, -0.4937760292030871079 ) ) ;
#19230=DIRECTION ( 'NONE',  ( -1.000000000000000000, 0.000000000000000000, 0.000000000000000000 ) ) ;
#19239=CIRCLE ( 'NONE', #17265, 0.4488493849861021068 ) ;
#19259=DIRECTION ( 'NONE',  ( -1.000000000000000000, -0.000000000000000000, -0.000000000000000000 ) ) ;
#19265=MANIFOLD_SOLID_BREP ( 'Chamfer1', #33228 ) ;
#19274=DIRECTION ( 'NONE',  ( 0.000000000000000000, 0.000000000000000000, -1.000000000000000000 ) ) ;
#19289=ORIENTED_EDGE ( 'NONE', *, *, #38123, .T. ) ;
#19290=EDGE_CURVE ( 'NONE', #4083, #1840, #26765, .T. ) ;
#19311=CIRCLE ( 'NONE', #33095, 0.5156329413417588547 ) ;
#19319=EDGE_CURVE ( 'NONE', #7253, #1152, #23281, .T. ) ;
#19328=CIRCLE ( 'NONE', #33108, 0.07999999999999996003 ) ;
#19344=CARTESIAN_POINT ( 'NONE',  ( -0.08000000000000000167, -1.622350287959229087, -0.009600792027532436754 ) ) ;
#19365=AXIS2_PLACEMENT_3D ( 'NONE', #35986, #16875, #17263 ) ;
#19369=VECTOR ( 'NONE', #32021, 39.37007874015748143 ) ;
#19376=CIRCLE ( 'NONE', #981, 0.06250000000000001388 ) ;
#19395=AXIS2_PLACEMENT_3D ( 'NONE', #34886, #26064, #25643 ) ;
#19420=DIRECTION ( 'NONE',  ( 0.000000000000000000, 0.000000000000000000, -1.000000000000000000 ) ) ;
#19433=ORIENTED_EDGE ( 'NONE', *, *, #16057, .F. ) ;
#19450=DIRECTION ( 'NONE',  ( -1.000000000000000000, -0.000000000000000000, -0.000000000000000000 ) ) ;
#19459=VECTOR ( 'NONE', #19519, 39.37007874015748854 ) ;
#19519=DIRECTION ( 'NONE',  ( -0.4999999999999981681, -0.6509737717187603634, 0.5711682313769322894 ) ) ;
#19529=DIRECTION ( 'NONE',  ( 0.000000000000000000, 0.000000000000000000, -1.000000000000000000 ) ) ;
#19560=CARTESIAN_POINT ( 'NONE',  ( -0.08000000000000000167, -2.183180860297908144, -0.5562760292030870524 ) ) ;
#19626=CARTESIAN_POINT ( 'NONE',  ( -0.08000000000000000167, -1.669835911085076674, -0.2333336242928227278 ) ) ;
#19630=EDGE_LOOP ( 'NONE', ( #18667, #29531, #40009, #23491 ) ) ;
#19677=ORIENTED_EDGE ( 'NONE', *, *, #39589, .T. ) ;
#19685=ORIENTED_EDGE ( 'NONE', *, *, #39339, .F. ) ;
#19705=LINE ( 'NONE', #16236, #8764 ) ;
#19710=EDGE_CURVE ( 'NONE', #34558, #12973, #19920, .T. ) ;
#19716=DIRECTION ( 'NONE',  ( 0.000000000000000000, 0.000000000000000000, -1.000000000000000000 ) ) ;
#19717=EDGE_LOOP ( 'NONE', ( #18307, #6774, #24665, #32247 ) ) ;
#19718=EDGE_LOOP ( 'NONE', ( #29908, #15534, #33184, #27954 ) ) ;
#19722=CARTESIAN_POINT ( 'NONE',  ( -0.02000000000000000042, -2.183180860297908144, -0.4937760292030871079 ) ) ;
#19729=EDGE_LOOP ( 'NONE', ( #30660, #30919, #25425, #6084 ) ) ;
#19738=ORIENTED_EDGE ( 'NONE', *, *, #24783, .T. ) ;
#19742=EDGE_CURVE ( 'NONE', #15898, #16107, #31100, .T. ) ;
#19752=CARTESIAN_POINT ( 'NONE',  ( -0.02000000000000000042, -1.717917452254872357, -0.2877234685858645613 ) ) ;
#19758=EDGE_CURVE ( 'NONE', #4083, #28686, #32401, .T. ) ;
#19767=CARTESIAN_POINT ( 'NONE',  ( -0.05464101615137786222, -2.196071624283071788, -0.8624000883860228894 ) ) ;
#19774=ORIENTED_EDGE ( 'NONE', *, *, #7210, .F. ) ;
#19779=CIRCLE ( 'NONE', #35540, 0.1400000000000009570 ) ;
#19789=DIRECTION ( 'NONE',  ( 1.000000000000000000, -0.000000000000000000, -0.000000000000000000 ) ) ;
#19808=EDGE_CURVE ( 'NONE', #40614, #8526, #40281, .T. ) ;
#19816=ORIENTED_EDGE ( 'NONE', *, *, #26622, .T. ) ;
#19821=VERTEX_POINT ( 'NONE', #26908 ) ;
#19830=CARTESIAN_POINT ( 'NONE',  ( -0.08000000000000000167, -2.183180860297908144, -0.4937760292030871079 ) ) ;
#19832=VECTOR ( 'NONE', #35071, 39.37007874015748143 ) ;
#19841=ORIENTED_EDGE ( 'NONE', *, *, #23252, .T. ) ;
#19842=AXIS2_PLACEMENT_3D ( 'NONE', #22204, #19100, #16015 ) ;
#19843=EDGE_CURVE ( 'NONE', #7871, #10115, #24430, .T. ) ;
#19853=AXIS2_PLACEMENT_3D ( 'NONE', #10332, #698, #16487 ) ;
#19861=EDGE_LOOP ( 'NONE', ( #6042, #21760, #23284, #34713 ) ) ;
#19913=CARTESIAN_POINT ( 'NONE',  ( -0.02000000000000000042, -2.616518742763782601, -0.2555225440839158368 ) ) ;
#19920=LINE ( 'NONE', #28964, #7441 ) ;
#19921=DIRECTION ( 'NONE',  ( -1.000000000000000000, -0.000000000000000000, -0.000000000000000000 ) ) ;
#19923=ORIENTED_EDGE ( 'NONE', *, *, #6279, .F. ) ;
#19950=DIRECTION ( 'NONE',  ( 0.000000000000000000, 0.000000000000000000, 1.000000000000000000 ) ) ;
#19961=CARTESIAN_POINT ( 'NONE',  ( -0.02000000000000000042, -2.023118915020511999, -0.4686803309516410221 ) ) ;
#20026=CIRCLE ( 'NONE', #25289, 0.07999999999999996003 ) ;
#20037=VERTEX_POINT ( 'NONE', #2552 ) ;
#20060=EDGE_CURVE ( 'NONE', #8808, #34243, #33406, .T. ) ;
#20083=ORIENTED_EDGE ( 'NONE', *, *, #27357, .F. ) ;
#20103=ORIENTED_EDGE ( 'NONE', *, *, #18331, .F. ) ;
#20111=EDGE_CURVE ( 'NONE', #37905, #5340, #25855, .T. ) ;
#20113=EDGE_LOOP ( 'NONE', ( #1921, #23734, #14223, #13953 ) ) ;
#20127=LINE ( 'NONE', #38215, #19459 ) ;
#20162=CARTESIAN_POINT ( 'NONE',  ( -0.05464101615137795243, -1.546789565643408526, -0.06332195561662121164 ) ) ;
#20183=LINE ( 'NONE', #38486, #34355 ) ;
#20187=ORIENTED_EDGE ( 'NONE', *, *, #28866, .T. ) ;
#20229=DIRECTION ( 'NONE',  ( -1.000000000000000000, -0.000000000000000000, -0.000000000000000000 ) ) ;
#20264=EDGE_LOOP ( 'NONE', ( #26972, #36621, #4938, #30814, #37941, #33400, #1324 ) ) ;
#20282=EDGE_CURVE ( 'NONE', #13057, #33645, #21422, .T. ) ;
#20335=DIRECTION ( 'NONE',  ( 0.000000000000000000, 0.000000000000000000, -1.000000000000000000 ) ) ;
#20345=CARTESIAN_POINT ( 'NONE',  ( -0.02000000000000000042, -1.622350287959229087, -0.08960079202753243321 ) ) ;
#20367=EDGE_CURVE ( 'NONE', #37987, #19134, #36374, .T. ) ;
#20396=CARTESIAN_POINT ( 'NONE',  ( -0.02000000000000000042, -2.320036485105098301, -0.2941690811493925528 ) ) ;
#20407=CARTESIAN_POINT ( 'NONE',  ( -0.02000000000000000042, -2.183180860297908144, -0.4937760292030871079 ) ) ;
#20408=LINE ( 'NONE', #4746, #30319 ) ;
#20412=DIRECTION ( 'NONE',  ( -0.8660254037844402619, -0.4607757839015039769, -0.1941279912067088165 ) ) ;
#20445=DIRECTION ( 'NONE',  ( -1.000000000000000000, -0.000000000000000000, -0.000000000000000000 ) ) ;
#20469=CIRCLE ( 'NONE', #10625, 0.08000000000000000167 ) ;
#20479=DIRECTION ( 'NONE',  ( -1.000000000000000000, -0.000000000000000000, -0.000000000000000000 ) ) ;
#20497=DIRECTION ( 'NONE',  ( 0.000000000000000000, 0.000000000000000000, 1.000000000000000000 ) ) ;
#20526=DIRECTION ( 'NONE',  ( 1.000000000000000000, 0.000000000000000000, 0.000000000000000000 ) ) ;
#20554=ORIENTED_EDGE ( 'NONE', *, *, #40365, .T. ) ;
#20561=ORIENTED_EDGE ( 'NONE', *, *, #4666, .F. ) ;
#20572=EDGE_CURVE ( 'NONE', #39409, #15916, #16254, .T. ) ;
#20582=DIRECTION ( 'NONE',  ( 0.000000000000000000, 0.000000000000000000, 1.000000000000000000 ) ) ;
#20601=AXIS2_PLACEMENT_3D ( 'NONE', #9931, #22502, #19420 ) ;
#20620=CONICAL_SURFACE ( 'NONE', #37045, 0.1400000000000005684, 1.047197551196600518 ) ;
#20631=DIRECTION ( 'NONE',  ( 1.000000000000000000, 0.000000000000000000, 0.000000000000000000 ) ) ;
#20637=CONICAL_SURFACE ( 'NONE', #33098, 0.5156329413417598539, 1.047197551196601184 ) ;
#20672=VERTEX_POINT ( 'NONE', #33474 ) ;
#20673=DIRECTION ( 'NONE',  ( -1.000000000000000000, -0.000000000000000000, -0.000000000000000000 ) ) ;
#20683=VECTOR ( 'NONE', #7802, 39.37007874015748143 ) ;
#20734=ADVANCED_FACE ( 'NONE', ( #14775 ), #9006, .F. ) ;
#20747=ORIENTED_EDGE ( 'NONE', *, *, #32509, .F. ) ;
#20755=EDGE_CURVE ( 'NONE', #24008, #7319, #21153, .T. ) ;
#20771=VERTEX_POINT ( 'NONE', #5494 ) ;
#20800=DIRECTION ( 'NONE',  ( 1.000000000000000000, 0.000000000000000000, 0.000000000000000000 ) ) ;
#20812=ORIENTED_EDGE ( 'NONE', *, *, #22464, .T. ) ;
#20820=CARTESIAN_POINT ( 'NONE',  ( -0.07999999999999998779, -1.984114763688379579, -0.7731012124309359912 ) ) ;
#20832=DIRECTION ( 'NONE',  ( 0.000000000000000000, -0.8063205929144885431, 0.5914787413272156735 ) ) ;
#20838=ADVANCED_FACE ( 'NONE', ( #25038 ), #10807, .T. ) ;
#20840=VECTOR ( 'NONE', #10627, 39.37007874015748143 ) ;
#20865=VERTEX_POINT ( 'NONE', #25872 ) ;
#20879=ORIENTED_EDGE ( 'NONE', *, *, #13765, .F. ) ;
#20892=DIRECTION ( 'NONE',  ( 0.4999999999999976685, 0.000000000000000000, -0.8660254037844400399 ) ) ;
#20900=ORIENTED_EDGE ( 'NONE', *, *, #28279, .T. ) ;
#20928=DIRECTION ( 'NONE',  ( 1.000000000000000000, 0.000000000000000000, 0.000000000000000000 ) ) ;
#20966=EDGE_CURVE ( 'NONE', #24008, #21212, #411, .T. ) ;
#20971=LINE ( 'NONE', #31028, #23094 ) ;
#20973=CARTESIAN_POINT ( 'NONE',  ( -0.05464101615137785528, -2.180132361182266720, -0.6941833704005058170 ) ) ;
#21012=ORIENTED_EDGE ( 'NONE', *, *, #12000, .F. ) ;
#21022=FACE_OUTER_BOUND ( 'NONE', #22082, .T. ) ;
#21027=DIRECTION ( 'NONE',  ( 0.000000000000000000, 0.000000000000000000, 1.000000000000000000 ) ) ;
#21034=DIRECTION ( 'NONE',  ( -1.000000000000000000, -0.000000000000000000, -0.000000000000000000 ) ) ;
#21036=DIRECTION ( 'NONE',  ( 0.000000000000000000, -6.829619984160655877E-15, -1.000000000000000000 ) ) ;
#21038=DIRECTION ( 'NONE',  ( 1.000000000000000000, 0.000000000000000000, 0.000000000000000000 ) ) ;
#21046=VERTEX_POINT ( 'NONE', #6709 ) ;
#21049=LINE ( 'NONE', #11176, #21080 ) ;
#21052=EDGE_CURVE ( 'NONE', #5057, #30904, #10013, .T. ) ;
#21064=ORIENTED_EDGE ( 'NONE', *, *, #33934, .F. ) ;
#21069=CARTESIAN_POINT ( 'NONE',  ( -0.05464101615137762630, -2.183180860297908144, -0.4937760292030871079 ) ) ;
#21079=DIRECTION ( 'NONE',  ( -1.000000000000000000, -0.000000000000000000, -0.000000000000000000 ) ) ;
#21080=VECTOR ( 'NONE', #14450, 39.37007874015748143 ) ;
#21082=ORIENTED_EDGE ( 'NONE', *, *, #31086, .T. ) ;
#21106=FACE_OUTER_BOUND ( 'NONE', #25753, .T. ) ;
#21107=ORIENTED_EDGE ( 'NONE', *, *, #25286, .T. ) ;
#21130=DIRECTION ( 'NONE',  ( 0.000000000000000000, 0.000000000000000000, -1.000000000000000000 ) ) ;
#21136=DIRECTION ( 'NONE',  ( -1.000000000000000000, 0.000000000000000000, 0.000000000000000000 ) ) ;
#21153=LINE ( 'NONE', #21973, #12741 ) ;
#21181=CIRCLE ( 'NONE', #10011, 0.08000000000000000167 ) ;
#21197=ORIENTED_EDGE ( 'NONE', *, *, #37694, .F. ) ;
#21202=VECTOR ( 'NONE', #20526, 39.37007874015748143 ) ;
#21208=CARTESIAN_POINT ( 'NONE',  ( -0.08000000000000000167, -2.177105168660885326, -0.2518349584362399862 ) ) ;
#21212=VERTEX_POINT ( 'NONE', #5046 ) ;
#21225=CARTESIAN_POINT ( 'NONE',  ( -0.02000000000000000042, -2.253856486606507836, -0.7252438489935795207 ) ) ;
#21250=LINE ( 'NONE', #18772, #15862 ) ;
#21261=DIRECTION ( 'NONE',  ( 1.000000000000000000, 0.000000000000000000, 0.000000000000000000 ) ) ;
#21281=DIRECTION ( 'NONE',  ( 1.000000000000000000, 0.000000000000000000, 0.000000000000000000 ) ) ;
#21287=EDGE_CURVE ( 'NONE', #33645, #1152, #26590, .T. ) ;
#21306=ORIENTED_EDGE ( 'NONE', *, *, #33369, .T. ) ;
#21313=EDGE_CURVE ( 'NONE', #15916, #16708, #15114, .T. ) ;
#21321=ORIENTED_EDGE ( 'NONE', *, *, #38433, .F. ) ;
#21330=CIRCLE ( 'NONE', #36432, 0.5088493849861029927 ) ;
#21358=DIRECTION ( 'NONE',  ( 1.000000000000000000, -0.000000000000000000, -0.000000000000000000 ) ) ;
#21361=VECTOR ( 'NONE', #29525, 39.37007874015748854 ) ;
#21373=ORIENTED_EDGE ( 'NONE', *, *, #2043, .F. ) ;
#21392=LINE ( 'NONE', #27140, #40062 ) ;
#21412=DIRECTION ( 'NONE',  ( 0.000000000000000000, 0.000000000000000000, -1.000000000000000000 ) ) ;
#21414=DIRECTION ( 'NONE',  ( 1.000000000000000000, 0.000000000000000000, 0.000000000000000000 ) ) ;
#21422=LINE ( 'NONE', #31062, #18644 ) ;
#21425=CIRCLE ( 'NONE', #6294, 0.08000000000000002942 ) ;
#21441=FACE_OUTER_BOUND ( 'NONE', #24914, .T. ) ;
#21471=EDGE_LOOP ( 'NONE', ( #13506, #12549, #9010, #37693, #15387, #32079, #14443, #20812, #29363 ) ) ;
#21477=ORIENTED_EDGE ( 'NONE', *, *, #12935, .F. ) ;
#21494=AXIS2_PLACEMENT_3D ( 'NONE', #21832, #33968, #5771 ) ;
#21582=ADVANCED_FACE ( 'NONE', ( #33742 ), #18117, .T. ) ;
#21623=DIRECTION ( 'NONE',  ( 0.000000000000000000, 0.000000000000000000, -1.000000000000000000 ) ) ;
#21685=CARTESIAN_POINT ( 'NONE',  ( -0.05464101615137796630, -2.183180860297908144, -0.4937760292030871079 ) ) ;
#21741=EDGE_CURVE ( 'NONE', #38795, #29445, #657, .T. ) ;
#21746=ADVANCED_FACE ( 'NONE', ( #31885 ), #3611, .F. ) ;
#21753=CARTESIAN_POINT ( 'NONE',  ( -0.02000000000000000042, -1.598492537578166672, -0.3371380022280838773 ) ) ;
#21760=ORIENTED_EDGE ( 'NONE', *, *, #22495, .T. ) ;
#21775=AXIS2_PLACEMENT_3D ( 'NONE', #7020, #10508, #13791 ) ;
#21782=DIRECTION ( 'NONE',  ( 0.000000000000000000, 0.000000000000000000, -1.000000000000000000 ) ) ;
#21792=AXIS2_PLACEMENT_3D ( 'NONE', #4091, #35189, #13154 ) ;
#21806=EDGE_LOOP ( 'NONE', ( #32166, #27070, #15608, #21373 ) ) ;
#21808=ORIENTED_EDGE ( 'NONE', *, *, #28599, .T. ) ;
#21828=ORIENTED_EDGE ( 'NONE', *, *, #39339, .T. ) ;
#21832=CARTESIAN_POINT ( 'NONE',  ( -0.02000000000000000042, -1.599201040860868339, 0.1642182323853691728 ) ) ;
#21835=AXIS2_PLACEMENT_3D ( 'NONE', #25373, #28844, #9300 ) ;
#21840=AXIS2_PLACEMENT_3D ( 'NONE', #9955, #947, #4183 ) ;
#21856=LINE ( 'NONE', #30893, #12302 ) ;
#21887=VECTOR ( 'NONE', #2855, 39.37007874015748854 ) ;
#21888=DIRECTION ( 'NONE',  ( 0.000000000000000000, 0.000000000000000000, -1.000000000000000000 ) ) ;
#21908=CARTESIAN_POINT ( 'NONE',  ( -0.05464101615137770263, -2.177105168660885326, -0.3318349584362400018 ) ) ;
#21912=ORIENTED_EDGE ( 'NONE', *, *, #1886, .F. ) ;
#21919=FACE_OUTER_BOUND ( 'NONE', #24058, .T. ) ;
#21928=AXIS2_PLACEMENT_3D ( 'NONE', #12662, #16785, #29115 ) ;
#21973=CARTESIAN_POINT ( 'NONE',  ( -0.02000000000000000042, -2.198867511061768809, -0.9423512173156428640 ) ) ;
#22039=DIRECTION ( 'NONE',  ( -1.000000000000000000, -0.000000000000000000, -0.000000000000000000 ) ) ;
#22045=ORIENTED_EDGE ( 'NONE', *, *, #34025, .T. ) ;
#22046=AXIS2_PLACEMENT_3D ( 'NONE', #11194, #7485, #36085 ) ;
#22074=DIRECTION ( 'NONE',  ( -0.4697114767686432213, -0.8828199865158355975, 0.000000000000000000 ) ) ;
#22082=EDGE_LOOP ( 'NONE', ( #22734, #35611, #5792, #35479 ) ) ;
#22084=ADVANCED_FACE ( 'NONE', ( #11649 ), #31184, .F. ) ;
#22103=AXIS2_PLACEMENT_3D ( 'NONE', #23190, #11436, #7918 ) ;
#22106=LINE ( 'NONE', #19198, #22689 ) ;
#22139=DIRECTION ( 'NONE',  ( 0.000000000000000000, 0.000000000000000000, 1.000000000000000000 ) ) ;
#22161=DIRECTION ( 'NONE',  ( 0.000000000000000000, 0.8063205929144885431, -0.5914787413272156735 ) ) ;
#22200=VERTEX_POINT ( 'NONE', #24611 ) ;
#22204=CARTESIAN_POINT ( 'NONE',  ( -0.02000000000000000042, -1.845925619402022155, -0.3444148183989317880 ) ) ;
#22223=AXIS2_PLACEMENT_3D ( 'NONE', #20396, #28274, #25198 ) ;
#22258=DIRECTION ( 'NONE',  ( 1.000000000000000000, 0.000000000000000000, 0.000000000000000000 ) ) ;
#22301=LENGTH_MEASURE_WITH_UNIT ( LENGTH_MEASURE( 0.02539999999999999897 ), #9732 );
#22323=CARTESIAN_POINT ( 'NONE',  ( -0.05464101615137762630, -2.023118915020511999, -0.4686803309516410221 ) ) ;
#22361=AXIS2_PLACEMENT_3D ( 'NONE', #30048, #23674, #1873 ) ;
#22366=CARTESIAN_POINT ( 'NONE',  ( -0.08000000000000000167, -1.622350287959229087, -0.08960079202753243321 ) ) ;
#22368=EDGE_CURVE ( 'NONE', #14209, #10794, #36846, .T. ) ;
#22387=CONICAL_SURFACE ( 'NONE', #4597, 0.1620173459747806799, 1.047197551196601184 ) ;
#22410=PLANE ( 'NONE',  #10711 ) ;
#22415=DIRECTION ( 'NONE',  ( -1.000000000000000000, -0.000000000000000000, -0.000000000000000000 ) ) ;
#22435=DIRECTION ( 'NONE',  ( -0.8660254037844400399, -0.3758398823372107178, 0.3297641321380319068 ) ) ;
#22446=CARTESIAN_POINT ( 'NONE',  ( -0.05464101615137770263, -2.320036485105098301, -0.2941690811493925528 ) ) ;
#22458=CARTESIAN_POINT ( 'NONE',  ( -0.02000000000000000042, -1.999693152383498873, -0.3073943322174664261 ) ) ;
#22464=EDGE_CURVE ( 'NONE', #39409, #14867, #27641, .T. ) ;
#22481=DIRECTION ( 'NONE',  ( 0.000000000000000000, 0.000000000000000000, -1.000000000000000000 ) ) ;
#22495=EDGE_CURVE ( 'NONE', #32357, #26267, #9917, .T. ) ;
#22502=DIRECTION ( 'NONE',  ( -1.000000000000000000, -0.000000000000000000, -0.000000000000000000 ) ) ;
#22504=DIRECTION ( 'NONE',  ( -1.000000000000000000, 0.000000000000000000, 0.000000000000000000 ) ) ;
#22522=VERTEX_POINT ( 'NONE', #10737 ) ;
#22524=ORIENTED_EDGE ( 'NONE', *, *, #28279, .F. ) ;
#22550=AXIS2_PLACEMENT_3D ( 'NONE', #40448, #25010, #15562 ) ;
#22559=VECTOR ( 'NONE', #28773, 39.37007874015748143 ) ;
#22564=LINE ( 'NONE', #35096, #29157 ) ;
#22572=CARTESIAN_POINT ( 'NONE',  ( -0.02000000000000000042, -2.577535374323032702, -0.2789082543815905035 ) ) ;
#22615=DIRECTION ( 'NONE',  ( 1.000000000000000000, 0.000000000000000000, 0.000000000000000000 ) ) ;
#22632=EDGE_LOOP ( 'NONE', ( #16003, #7812, #31991, #31115 ) ) ;
#22681=ORIENTED_EDGE ( 'NONE', *, *, #19710, .F. ) ;
#22688=EDGE_LOOP ( 'NONE', ( #15128, #24596, #25658, #27223 ) ) ;
#22689=VECTOR ( 'NONE', #40587, 39.37007874015748143 ) ;
#22695=CYLINDRICAL_SURFACE ( 'NONE', #29820, 0.06250000000000001388 ) ;
#22726=ORIENTED_EDGE ( 'NONE', *, *, #24087, .F. ) ;
#22734=ORIENTED_EDGE ( 'NONE', *, *, #23255, .F. ) ;
#22760=CIRCLE ( 'NONE', #37833, 0.08000000000000002942 ) ;
#22789=FACE_OUTER_BOUND ( 'NONE', #10523, .T. ) ;
#22797=ORIENTED_EDGE ( 'NONE', *, *, #28339, .T. ) ;
#22802=EDGE_LOOP ( 'NONE', ( #3094, #21197, #24864, #29758 ) ) ;
#22836=DIRECTION ( 'NONE',  ( 0.000000000000000000, 1.686145379822168900E-15, -1.000000000000000000 ) ) ;
#22838=VECTOR ( 'NONE', #19167, 39.37007874015748143 ) ;
#22844=ORIENTED_EDGE ( 'NONE', *, *, #33901, .T. ) ;
#22850=ORIENTED_EDGE ( 'NONE', *, *, #2018, .F. ) ;
#22914=DIRECTION ( 'NONE',  ( 0.000000000000000000, -1.951319995474454795E-15, -1.000000000000000000 ) ) ;
#22926=DIRECTION ( 'NONE',  ( 1.000000000000000000, 0.000000000000000000, 0.000000000000000000 ) ) ;
#22933=ORIENTED_EDGE ( 'NONE', *, *, #1657, .T. ) ;
#22934=DIRECTION ( 'NONE',  ( -1.000000000000000000, 0.000000000000000000, 0.000000000000000000 ) ) ;
#22952=CARTESIAN_POINT ( 'NONE',  ( -0.05464101615137770263, -2.177105168660885326, -0.2518349584362399862 ) ) ;
#22980=ORIENTED_EDGE ( 'NONE', *, *, #10314, .F. ) ;
#22988=VERTEX_POINT ( 'NONE', #24151 ) ;
#23047=FACE_OUTER_BOUND ( 'NONE', #35335, .T. ) ;
#23055=CARTESIAN_POINT ( 'NONE',  ( -0.05464101615137795936, -1.518907846805490403, -0.1889969338327479598 ) ) ;
#23065=ORIENTED_EDGE ( 'NONE', *, *, #12716, .F. ) ;
#23072=EDGE_CURVE ( 'NONE', #14616, #34947, #27825, .T. ) ;
#23085=EDGE_LOOP ( 'NONE', ( #15691, #34549 ) ) ;
#23087=FACE_OUTER_BOUND ( 'NONE', #40426, .T. ) ;
#23090=CIRCLE ( 'NONE', #25726, 0.07999999999999996003 ) ;
#23094=VECTOR ( 'NONE', #17861, 39.37007874015748143 ) ;
#23097=CIRCLE ( 'NONE', #24412, 0.1020173459747799466 ) ;
#23112=( NAMED_UNIT ( * ) SI_UNIT ( $, .STERADIAN. ) SOLID_ANGLE_UNIT ( ) );
#23125=ORIENTED_EDGE ( 'NONE', *, *, #26982, .F. ) ;
#23155=AXIS2_PLACEMENT_3D ( 'NONE', #20407, #32940, #4745 ) ;
#23158=CONICAL_SURFACE ( 'NONE', #21840, 0.01999999999999924061, 1.047197551196600962 ) ;
#23173=CARTESIAN_POINT ( 'NONE',  ( -0.02000000000000000042, -2.183180860297908144, -0.3917586832283071474 ) ) ;
#23179=ORIENTED_EDGE ( 'NONE', *, *, #15343, .T. ) ;
#23186=AXIS2_PLACEMENT_3D ( 'NONE', #9857, #18937, #6977 ) ;
#23190=CARTESIAN_POINT ( 'NONE',  ( -0.02000000000000000042, -2.070343076906777213, -0.2454056712452573896 ) ) ;
#23192=ORIENTED_EDGE ( 'NONE', *, *, #38880, .T. ) ;
#23194=EDGE_LOOP ( 'NONE', ( #14446, #27586, #35132, #30059 ) ) ;
#23202=CARTESIAN_POINT ( 'NONE',  ( -0.02000000000000000042, -2.180619779672576364, -0.3917908354455199582 ) ) ;
#23214=CIRCLE ( 'NONE', #39629, 0.5156329413417597429 ) ;
#23217=CARTESIAN_POINT ( 'NONE',  ( -0.02000000000000000042, -2.240869484095992181, -0.4096358986825019977 ) ) ;
#23252=EDGE_CURVE ( 'NONE', #29445, #4305, #39484, .T. ) ;
#23255=EDGE_CURVE ( 'NONE', #29395, #12860, #7203, .T. ) ;
#23267=DIRECTION ( 'NONE',  ( 1.000000000000000000, -0.000000000000000000, -0.000000000000000000 ) ) ;
#23274=FACE_OUTER_BOUND ( 'NONE', #13343, .T. ) ;
#23281=LINE ( 'NONE', #7194, #34992 ) ;
#23284=ORIENTED_EDGE ( 'NONE', *, *, #40365, .F. ) ;
#23298=DIRECTION ( 'NONE',  ( -1.000000000000000000, 0.000000000000000000, 0.000000000000000000 ) ) ;
#23327=LINE ( 'NONE', #36239, #35029 ) ;
#23332=AXIS2_PLACEMENT_3D ( 'NONE', #24010, #11043, #17800 ) ;
#23343=ORIENTED_EDGE ( 'NONE', *, *, #33369, .F. ) ;
#23355=EDGE_CURVE ( 'NONE', #16485, #7866, #20469, .T. ) ;
#23369=DIRECTION ( 'NONE',  ( 0.000000000000000000, 0.000000000000000000, -1.000000000000000000 ) ) ;
#23385=DIRECTION ( 'NONE',  ( 1.000000000000000000, 0.000000000000000000, 0.000000000000000000 ) ) ;
#23395=CARTESIAN_POINT ( 'NONE',  ( -0.02000000000000000042, -1.622350287959229087, -0.08960079202753243321 ) ) ;
#23398=DIMENSIONAL_EXPONENTS ( 1.000000000000000000, 0.000000000000000000, 0.000000000000000000, 0.000000000000000000, 0.000000000000000000, 0.000000000000000000, 0.000000000000000000 ) ;
#23441=DIRECTION ( 'NONE',  ( 0.000000000000000000, 0.000000000000000000, -1.000000000000000000 ) ) ;
#23451=ORIENTED_EDGE ( 'NONE', *, *, #8220, .F. ) ;
#23488=LINE ( 'NONE', #17497, #29661 ) ;
#23491=ORIENTED_EDGE ( 'NONE', *, *, #6996, .F. ) ;
#23493=VERTEX_POINT ( 'NONE', #22572 ) ;
#23496=ORIENTED_EDGE ( 'NONE', *, *, #30846, .T. ) ;
#23517=LINE ( 'NONE', #915, #27748 ) ;
#23528=EDGE_CURVE ( 'NONE', #29395, #18399, #15242, .T. ) ;
#23547=VERTEX_POINT ( 'NONE', #17937 ) ;
#23582=ADVANCED_FACE ( 'NONE', ( #5375 ), #10214, .T. ) ;
#23628=DIRECTION ( 'NONE',  ( -1.000000000000000000, -0.000000000000000000, -0.000000000000000000 ) ) ;
#23653=CARTESIAN_POINT ( 'NONE',  ( -0.08000000000000000167, -2.551729310907437043, -0.4286726180052709001 ) ) ;
#23674=DIRECTION ( 'NONE',  ( 1.000000000000000000, -0.000000000000000000, -0.000000000000000000 ) ) ;
#23696=DIRECTION ( 'NONE',  ( -1.000000000000000000, 0.000000000000000000, 0.000000000000000000 ) ) ;
#23734=ORIENTED_EDGE ( 'NONE', *, *, #35783, .T. ) ;
#23741=ORIENTED_EDGE ( 'NONE', *, *, #2960, .F. ) ;
#23753=ADVANCED_FACE ( 'NONE', ( #28216 ), #83, .F. ) ;
#23762=DIRECTION ( 'NONE',  ( -1.000000000000000000, -0.000000000000000000, -0.000000000000000000 ) ) ;
#23807=EDGE_CURVE ( 'NONE', #34947, #27531, #11952, .T. ) ;
#23820=DIRECTION ( 'NONE',  ( 0.000000000000000000, 0.000000000000000000, -1.000000000000000000 ) ) ;
#23822=DIRECTION ( 'NONE',  ( 1.000000000000000000, -0.000000000000000000, -0.000000000000000000 ) ) ;
#23823=CIRCLE ( 'NONE', #39528, 0.07999999999999996003 ) ;
#23827=CARTESIAN_POINT ( 'NONE',  ( -0.02000000000000000042, -2.070343076906777213, -0.2454056712452573896 ) ) ;
#23837=ORIENTED_EDGE ( 'NONE', *, *, #29419, .T. ) ;
#23848=DIRECTION ( 'NONE',  ( 0.000000000000000000, 0.000000000000000000, -1.000000000000000000 ) ) ;
#23860=FACE_OUTER_BOUND ( 'NONE', #32116, .T. ) ;
#23865=CIRCLE ( 'NONE', #14642, 0.01999999999999927530 ) ;
#23874=ADVANCED_FACE ( 'NONE', ( #10324 ), #16689, .F. ) ;
#23876=EDGE_CURVE ( 'NONE', #13895, #3745, #1092, .T. ) ;
#23878=CARTESIAN_POINT ( 'NONE',  ( -0.05464101615137773038, -2.626773565144302935, -0.1926934094652516249 ) ) ;
#23993=EDGE_CURVE ( 'NONE', #24718, #4481, #33324, .T. ) ;
#23997=PLANE ( 'NONE',  #31583 ) ;
#24002=DIRECTION ( 'NONE',  ( 1.000000000000000000, -0.000000000000000000, -0.000000000000000000 ) ) ;
#24008=VERTEX_POINT ( 'NONE', #39701 ) ;
#24010=CARTESIAN_POINT ( 'NONE',  ( -0.02000000000000000042, -1.646519645934556131, -0.1171471737359304072 ) ) ;
#24058=EDGE_LOOP ( 'NONE', ( #30291, #17618, #32471, #15924 ) ) ;
#24087=EDGE_CURVE ( 'NONE', #641, #20865, #31056, .T. ) ;
#24093=LINE ( 'NONE', #11724, #17085 ) ;
#24095=ORIENTED_EDGE ( 'NONE', *, *, #9883, .T. ) ;
#24101=CARTESIAN_POINT ( 'NONE',  ( -0.05464101615137787610, -2.551729310907437043, -0.4286726180052709001 ) ) ;
#24118=ORIENTED_EDGE ( 'NONE', *, *, #32849, .F. ) ;
#24129=VECTOR ( 'NONE', #9741, 39.37007874015748854 ) ;
#24131=CARTESIAN_POINT ( 'NONE',  ( -0.05464101615137762630, -2.058305985490972212, -0.5970033804171128722 ) ) ;
#24142=CARTESIAN_POINT ( 'NONE',  ( -0.05464101615137770263, -2.177105168660885326, -0.2518349584362399862 ) ) ;
#24146=EDGE_LOOP ( 'NONE', ( #36202, #8346, #38288, #39927 ) ) ;
#24151=CARTESIAN_POINT ( 'NONE',  ( -0.08000000000000000167, -2.122347498858831116, -0.8313396097929490747 ) ) ;
#24184=DIRECTION ( 'NONE',  ( 0.000000000000000000, 0.000000000000000000, -1.000000000000000000 ) ) ;
#24227=PLANE ( 'NONE',  #24533 ) ;
#24269=CARTESIAN_POINT ( 'NONE',  ( -0.02000000000000000042, -2.297142231534299306, -0.5217974784625020179 ) ) ;
#24291=DIRECTION ( 'NONE',  ( -1.000000000000000000, -0.000000000000000000, -0.000000000000000000 ) ) ;
#24341=DIRECTION ( 'NONE',  ( 0.000000000000000000, 0.000000000000000000, -1.000000000000000000 ) ) ;
#24374=AXIS2_PLACEMENT_3D ( 'NONE', #8477, #3131, #30496 ) ;
#24412=AXIS2_PLACEMENT_3D ( 'NONE', #192, #37787, #3427 ) ;
#24414=AXIS2_PLACEMENT_3D ( 'NONE', #3576, #28464, #339 ) ;
#24430=LINE ( 'NONE', #39440, #38308 ) ;
#24465=AXIS2_PLACEMENT_3D ( 'NONE', #30254, #14624, #39727 ) ;
#24475=LINE ( 'NONE', #30442, #922 ) ;
#24492=ADVANCED_FACE ( 'NONE', ( #22789 ), #22387, .T. ) ;
#24533=AXIS2_PLACEMENT_3D ( 'NONE', #23827, #39244, #36349 ) ;
#24536=AXIS2_PLACEMENT_3D ( 'NONE', #39942, #40134, #21027 ) ;
#24546=ORIENTED_EDGE ( 'NONE', *, *, #38802, .T. ) ;
#24559=CARTESIAN_POINT ( 'NONE',  ( -0.02000000000000000042, -1.761115123485013534, -0.1975702831323159492 ) ) ;
#24595=ORIENTED_EDGE ( 'NONE', *, *, #33881, .F. ) ;
#24596=ORIENTED_EDGE ( 'NONE', *, *, #38360, .T. ) ;
#24611=CARTESIAN_POINT ( 'NONE',  ( -0.08000000000000000167, -2.542046649843399564, -0.2305290188067205259 ) ) ;
#24617=CIRCLE ( 'NONE', #12770, 0.07999999999999996003 ) ;
#24621=AXIS2_PLACEMENT_3D ( 'NONE', #33872, #2406, #18637 ) ;
#24626=AXIS2_PLACEMENT_3D ( 'NONE', #13697, #26264, #29539 ) ;
#24628=DIRECTION ( 'NONE',  ( -1.000000000000000000, -0.000000000000000000, -0.000000000000000000 ) ) ;
#24647=EDGE_CURVE ( 'NONE', #20771, #30911, #39595, .T. ) ;
#24665=ORIENTED_EDGE ( 'NONE', *, *, #2018, .T. ) ;
#24674=ORIENTED_EDGE ( 'NONE', *, *, #18841, .F. ) ;
#24706=VECTOR ( 'NONE', #12907, 39.37007874015748143 ) ;
#24718=VERTEX_POINT ( 'NONE', #39811 ) ;
#24736=ADVANCED_FACE ( 'NONE', ( #12244 ), #23997, .F. ) ;
#24747=ORIENTED_EDGE ( 'NONE', *, *, #1882, .T. ) ;
#24761=CARTESIAN_POINT ( 'NONE',  ( -0.05464101615137762630, -1.910390638264138685, -0.7420407338378623985 ) ) ;
#24772=ORIENTED_EDGE ( 'NONE', *, *, #34264, .T. ) ;
#24783=EDGE_CURVE ( 'NONE', #33509, #19821, #2695, .T. ) ;
#24819=DIRECTION ( 'NONE',  ( 1.000000000000000000, 0.000000000000000000, 0.000000000000000000 ) ) ;
#24830=ADVANCED_FACE ( 'NONE', ( #21919 ), #36162, .F. ) ;
#24839=DIRECTION ( 'NONE',  ( 0.000000000000000000, 0.6595282642760672553, 0.7516797646744243222 ) ) ;
#24854=CARTESIAN_POINT ( 'NONE',  ( -0.05464101615137761936, -1.906060000575976021, -0.2916525572568466340 ) ) ;
#24864=ORIENTED_EDGE ( 'NONE', *, *, #19319, .F. ) ;
#24865=ORIENTED_EDGE ( 'NONE', *, *, #27552, .F. ) ;
#24897=ORIENTED_EDGE ( 'NONE', *, *, #30569, .F. ) ;
#24902=CARTESIAN_POINT ( 'NONE',  ( -0.02000000000000000042, -2.183180860297908144, -0.3917586832283071474 ) ) ;
#24914=EDGE_LOOP ( 'NONE', ( #135, #38445, #23125, #14465 ) ) ;
#24941=DIRECTION ( 'NONE',  ( 0.000000000000000000, -0.3882559824134196313, 0.9215515678030125057 ) ) ;
#24942=ORIENTED_EDGE ( 'NONE', *, *, #20367, .F. ) ;
#24963=FACE_OUTER_BOUND ( 'NONE', #36485, .T. ) ;
#25007=EDGE_CURVE ( 'NONE', #16107, #8744, #21049, .T. ) ;
#25010=DIRECTION ( 'NONE',  ( 0.000000000000000000, 0.7516797646744247663, -0.6595282642760668113 ) ) ;
#25024=ORIENTED_EDGE ( 'NONE', *, *, #19843, .F. ) ;
#25038=FACE_OUTER_BOUND ( 'NONE', #18309, .T. ) ;
#25039=FACE_OUTER_BOUND ( 'NONE', #1282, .T. ) ;
#25048=AXIS2_PLACEMENT_3D ( 'NONE', #19830, #38740, #16757 ) ;
#25057=ORIENTED_EDGE ( 'NONE', *, *, #20060, .F. ) ;
#25060=ORIENTED_EDGE ( 'NONE', *, *, #26320, .T. ) ;
#25067=CIRCLE ( 'NONE', #7293, 0.08000000000000000167 ) ;
#25074=CIRCLE ( 'NONE', #21792, 0.07999999999999996003 ) ;
#25118=EDGE_CURVE ( 'NONE', #18164, #26070, #34867, .T. ) ;
#25125=LINE ( 'NONE', #2703, #416 ) ;
#25137=DIRECTION ( 'NONE',  ( -0.8660254037844397068, 0.4607757839015044210, 0.1941279912067096214 ) ) ;
#25172=DIRECTION ( 'NONE',  ( 0.000000000000000000, 0.000000000000000000, 1.000000000000000000 ) ) ;
#25186=ORIENTED_EDGE ( 'NONE', *, *, #23528, .F. ) ;
#25195=DIRECTION ( 'NONE',  ( 0.000000000000000000, 0.7516797646744242112, -0.6595282642760673664 ) ) ;
#25198=DIRECTION ( 'NONE',  ( 0.000000000000000000, 0.000000000000000000, -1.000000000000000000 ) ) ;
#25254=DIRECTION ( 'NONE',  ( 0.000000000000000000, 0.000000000000000000, -1.000000000000000000 ) ) ;
#25283=CARTESIAN_POINT ( 'NONE',  ( -0.02000000000000000042, -2.196538720661423749, -0.6552417777791260667 ) ) ;
#25286=EDGE_CURVE ( 'NONE', #14004, #18990, #23090, .T. ) ;
#25289=AXIS2_PLACEMENT_3D ( 'NONE', #31195, #20928, #33449 ) ;
#25373=CARTESIAN_POINT ( 'NONE',  ( -0.05464101615137787610, -2.183180860297908144, -0.4937760292030871079 ) ) ;
#25378=DIRECTION ( 'NONE',  ( 1.000000000000000000, 0.000000000000000000, 0.000000000000000000 ) ) ;
#25402=CARTESIAN_POINT ( 'NONE',  ( -0.08000000000000000167, -1.699711333021935777, -0.9366211149475224262 ) ) ;
#25418=ORIENTED_EDGE ( 'NONE', *, *, #40125, .T. ) ;
#25425=ORIENTED_EDGE ( 'NONE', *, *, #31326, .T. ) ;
#25436=CARTESIAN_POINT ( 'NONE',  ( -0.02000000000000000042, -2.092549851682985018, -0.5406114768595331466 ) ) ;
#25448=CARTESIAN_POINT ( 'NONE',  ( -0.02000000000000000042, -2.070343076906777213, -0.2454056712452573896 ) ) ;
#25512=FACE_OUTER_BOUND ( 'NONE', #22802, .T. ) ;
#25525=ORIENTED_EDGE ( 'NONE', *, *, #274, .F. ) ;
#25556=ORIENTED_EDGE ( 'NONE', *, *, #9802, .T. ) ;
#25565=ORIENTED_EDGE ( 'NONE', *, *, #30846, .F. ) ;
#25566=EDGE_CURVE ( 'NONE', #20672, #21212, #19779, .T. ) ;
#25625=FACE_OUTER_BOUND ( 'NONE', #33685, .T. ) ;
#25643=DIRECTION ( 'NONE',  ( 0.000000000000000000, 0.000000000000000000, -1.000000000000000000 ) ) ;
#25658=ORIENTED_EDGE ( 'NONE', *, *, #31377, .T. ) ;
#25665=DIRECTION ( 'NONE',  ( 0.000000000000000000, -1.951319995474460317E-15, -1.000000000000000000 ) ) ;
#25667=VECTOR ( 'NONE', #30230, 39.37007874015748854 ) ;
#25677=FACE_OUTER_BOUND ( 'NONE', #5900, .T. ) ;
#25698=VERTEX_POINT ( 'NONE', #17199 ) ;
#25717=ORIENTED_EDGE ( 'NONE', *, *, #11664, .T. ) ;
#25726=AXIS2_PLACEMENT_3D ( 'NONE', #32470, #15277, #27832 ) ;
#25735=CIRCLE ( 'NONE', #24414, 0.01999999999999927530 ) ;
#25753=EDGE_LOOP ( 'NONE', ( #2173, #33144, #26884, #20879 ) ) ;
#25764=VERTEX_POINT ( 'NONE', #7308 ) ;
#25771=CONICAL_SURFACE ( 'NONE', #4736, 0.01999999999999927530, 1.047197551196601184 ) ;
#25789=DIRECTION ( 'NONE',  ( 0.000000000000000000, 0.000000000000000000, 1.000000000000000000 ) ) ;
#25808=VERTEX_POINT ( 'NONE', #1384 ) ;
#25814=ORIENTED_EDGE ( 'NONE', *, *, #274, .T. ) ;
#25815=DIRECTION ( 'NONE',  ( 1.000000000000000000, -0.000000000000000000, -0.000000000000000000 ) ) ;
#25818=CIRCLE ( 'NONE', #31060, 0.1400000000000013456 ) ;
#25836=AXIS2_PLACEMENT_3D ( 'NONE', #27310, #5865, #37161 ) ;
#25838=CARTESIAN_POINT ( 'NONE',  ( -0.02000000000000000042, -2.177105168660885326, -0.3918349584362407212 ) ) ;
#25855=CIRCLE ( 'NONE', #7466, 0.5543128707267515054 ) ;
#25863=ORIENTED_EDGE ( 'NONE', *, *, #34778, .F. ) ;
#25865=ADVANCED_FACE ( 'NONE', ( #4835 ), #13894, .T. ) ;
#25872=CARTESIAN_POINT ( 'NONE',  ( -0.05464101615137769569, -2.274798198814180772, -0.3601501197397404264 ) ) ;
#25883=DIRECTION ( 'NONE',  ( -1.000000000000000000, 0.000000000000000000, 0.000000000000000000 ) ) ;
#25894=DIRECTION ( 'NONE',  ( -0.4999999999999970024, 0.7723146731083251337, 0.3918291026730708615 ) ) ;
#25918=AXIS2_PLACEMENT_3D ( 'NONE', #2820, #37370, #9181 ) ;
#25938=CARTESIAN_POINT ( 'NONE',  ( -0.05464101615137762630, -2.032088213807425880, -0.4352898549974345555 ) ) ;
#25950=CIRCLE ( 'NONE', #3569, 0.1620173459747806799 ) ;
#25971=VECTOR ( 'NONE', #5448, 39.37007874015748143 ) ;
#25976=EDGE_LOOP ( 'NONE', ( #16814, #15071, #9563, #26280 ) ) ;
#26017=CARTESIAN_POINT ( 'NONE',  ( -0.02000000000000000042, -2.039407857756560638, -0.7963965713757412690 ) ) ;
#26025=CARTESIAN_POINT ( 'NONE',  ( -0.02000000000000000042, -2.589364949149576933, -0.2950346662398796171 ) ) ;
#26032=ADVANCED_FACE ( 'NONE', ( #21106 ), #33859, .F. ) ;
#26042=ADVANCED_FACE ( 'NONE', ( #30471 ), #26398, .T. ) ;
#26049=CARTESIAN_POINT ( 'NONE',  ( -0.02000000000000000042, -1.622350287959229087, -0.08960079202753243321 ) ) ;
#26064=DIRECTION ( 'NONE',  ( 1.000000000000000000, 0.000000000000000000, 0.000000000000000000 ) ) ;
#26070=VERTEX_POINT ( 'NONE', #36641 ) ;
#26148=DIRECTION ( 'NONE',  ( 0.000000000000000000, -0.8585432690668223232, 0.5127411190260187102 ) ) ;
#26170=EDGE_LOOP ( 'NONE', ( #25024, #33994, #5062, #21477 ) ) ;
#26183=CARTESIAN_POINT ( 'NONE',  ( -0.08000000000000000167, -2.626773565144302935, -0.1926934094652516249 ) ) ;
#26195=( NAMED_UNIT ( * ) PLANE_ANGLE_UNIT ( ) SI_UNIT ( $, .RADIAN. ) );
#26213=CARTESIAN_POINT ( 'NONE',  ( -0.02000000000000000042, -2.589364949149576933, -0.2950346662398796171 ) ) ;
#26241=ORIENTED_EDGE ( 'NONE', *, *, #35143, .F. ) ;
#26242=EDGE_CURVE ( 'NONE', #2801, #15916, #25074, .T. ) ;
#26264=DIRECTION ( 'NONE',  ( -1.000000000000000000, -0.000000000000000000, -0.000000000000000000 ) ) ;
#26267=VERTEX_POINT ( 'NONE', #19560 ) ;
#26270=ORIENTED_EDGE ( 'NONE', *, *, #6439, .F. ) ;
#26280=ORIENTED_EDGE ( 'NONE', *, *, #31542, .F. ) ;
#26286=DIRECTION ( 'NONE',  ( -1.000000000000000000, -0.000000000000000000, -0.000000000000000000 ) ) ;
#26291=LINE ( 'NONE', #35347, #22559 ) ;
#26309=DIRECTION ( 'NONE',  ( 0.000000000000000000, 0.000000000000000000, -1.000000000000000000 ) ) ;
#26311=VECTOR ( 'NONE', #9702, 39.37007874015748143 ) ;
#26320=EDGE_CURVE ( 'NONE', #15674, #8526, #20408, .T. ) ;
#26326=ORIENTED_EDGE ( 'NONE', *, *, #25286, .F. ) ;
#26355=ORIENTED_EDGE ( 'NONE', *, *, #23355, .F. ) ;
#26388=CARTESIAN_POINT ( 'NONE',  ( -0.08000000000000000167, -2.183180860297908144, -0.4937760292030871079 ) ) ;
#26398=CONICAL_SURFACE ( 'NONE', #34252, 0.1020173459747799466, 1.047197551196601184 ) ;
#26409=ORIENTED_EDGE ( 'NONE', *, *, #33901, .F. ) ;
#26413=ORIENTED_EDGE ( 'NONE', *, *, #21287, .F. ) ;
#26430=CARTESIAN_POINT ( 'NONE',  ( -0.08000000000000000167, -1.845925619402022155, -0.3444148183989317880 ) ) ;
#26451=AXIS2_PLACEMENT_3D ( 'NONE', #29269, #35843, #10747 ) ;
#26486=CARTESIAN_POINT ( 'NONE',  ( -0.02000000000000000042, -2.321277022828569958, -0.5785054236952983375 ) ) ;
#26496=CARTESIAN_POINT ( 'NONE',  ( -0.02000000000000000042, -1.599201040860868339, 0.1842182323853684411 ) ) ;
#26509=VERTEX_POINT ( 'NONE', #31300 ) ;
#26522=ORIENTED_EDGE ( 'NONE', *, *, #18042, .F. ) ;
#26533=DIRECTION ( 'NONE',  ( -1.000000000000000000, 0.000000000000000000, 0.000000000000000000 ) ) ;
#26537=CYLINDRICAL_SURFACE ( 'NONE', #7553, 0.5543128707267515054 ) ;
#26567=ORIENTED_EDGE ( 'NONE', *, *, #19758, .F. ) ;
#26577=DIRECTION ( 'NONE',  ( 0.000000000000000000, 0.000000000000000000, -1.000000000000000000 ) ) ;
#26584=CIRCLE ( 'NONE', #24621, 0.07999999999999996003 ) ;
#26590=CIRCLE ( 'NONE', #24626, 0.1400000000000007627 ) ;
#26621=AXIS2_PLACEMENT_3D ( 'NONE', #3890, #35377, #13361 ) ;
#26622=EDGE_CURVE ( 'NONE', #13057, #20865, #23823, .T. ) ;
#26650=VECTOR ( 'NONE', #2738, 39.37007874015748854 ) ;
#26706=AXIS2_PLACEMENT_3D ( 'NONE', #35981, #7366, #17258 ) ;
#26715=VECTOR ( 'NONE', #9068, 39.37007874015748854 ) ;
#26735=ORIENTED_EDGE ( 'NONE', *, *, #8697, .T. ) ;
#26765=LINE ( 'NONE', #32908, #15972 ) ;
#26788=LINE ( 'NONE', #20820, #28367 ) ;
#26830=DIRECTION ( 'NONE',  ( 0.000000000000000000, 0.000000000000000000, 1.000000000000000000 ) ) ;
#26845=EDGE_CURVE ( 'NONE', #2801, #39344, #8403, .T. ) ;
#26853=DIRECTION ( 'NONE',  ( 0.000000000000000000, 0.000000000000000000, -1.000000000000000000 ) ) ;
#26870=CARTESIAN_POINT ( 'NONE',  ( -0.02000000000000000042, -2.183180860297908144, -0.4937760292030871079 ) ) ;
#26873=DIRECTION ( 'NONE',  ( 0.000000000000000000, 0.000000000000000000, 1.000000000000000000 ) ) ;
#26875=ORIENTED_EDGE ( 'NONE', *, *, #28339, .F. ) ;
#26884=ORIENTED_EDGE ( 'NONE', *, *, #12737, .F. ) ;
#26904=FACE_BOUND ( 'NONE', #14520, .T. ) ;
#26908=CARTESIAN_POINT ( 'NONE',  ( -0.02000000000000000042, -2.266124458208340187, -0.5531721439363799231 ) ) ;
#26910=CARTESIAN_POINT ( 'NONE',  ( -0.02000000000000000042, -2.297142231534299306, -0.5217974784625020179 ) ) ;
#26920=ORIENTED_EDGE ( 'NONE', *, *, #19843, .T. ) ;
#26930=EDGE_LOOP ( 'NONE', ( #37023, #17889, #12821, #34134 ) ) ;
#26951=AXIS2_PLACEMENT_3D ( 'NONE', #7401, #3310, #29235 ) ;
#26972=ORIENTED_EDGE ( 'NONE', *, *, #35143, .T. ) ;
#26982=EDGE_CURVE ( 'NONE', #34243, #12973, #32305, .T. ) ;
#27023=CARTESIAN_POINT ( 'NONE',  ( -0.05464101615137762630, -2.032088213807425880, -0.4352898549974345555 ) ) ;
#27036=FACE_OUTER_BOUND ( 'NONE', #31827, .T. ) ;
#27070=ORIENTED_EDGE ( 'NONE', *, *, #14278, .F. ) ;
#27071=ORIENTED_EDGE ( 'NONE', *, *, #12000, .T. ) ;
#27083=DIRECTION ( 'NONE',  ( -0.4999999999999972244, 0.02174101728960634375, 0.8657524635640466704 ) ) ;
#27096=CARTESIAN_POINT ( 'NONE',  ( -0.05464101615137773038, -2.585754275622221154, -0.2040099479399058446 ) ) ;
#27109=ADVANCED_FACE ( 'NONE', ( #25677 ), #35137, .F. ) ;
#27117=CIRCLE ( 'NONE', #25836, 0.08000000000000002942 ) ;
#27138=VERTEX_POINT ( 'NONE', #3664 ) ;
#27140=CARTESIAN_POINT ( 'NONE',  ( -0.05464101615137786222, -2.122347498858831116, -0.8313396097929491857 ) ) ;
#27198=LINE ( 'NONE', #33976, #8234 ) ;
#27212=AXIS2_PLACEMENT_3D ( 'NONE', #28091, #35227, #35415 ) ;
#27216=ORIENTED_EDGE ( 'NONE', *, *, #10405, .T. ) ;
#27219=AXIS2_PLACEMENT_3D ( 'NONE', #19722, #1432, #38642 ) ;
#27223=ORIENTED_EDGE ( 'NONE', *, *, #19142, .T. ) ;
#27224=CARTESIAN_POINT ( 'NONE',  ( -0.02000000000000000042, -1.910390638264138685, -0.7420407338378623985 ) ) ;
#27227=EDGE_LOOP ( 'NONE', ( #35860, #32262, #17518, #3928, #15214, #30412, #6043, #21306, #32220 ) ) ;
#27235=CYLINDRICAL_SURFACE ( 'NONE', #30498, 0.08000000000000000167 ) ;
#27241=CIRCLE ( 'NONE', #35133, 0.07999999999999996003 ) ;
#27258=AXIS2_PLACEMENT_3D ( 'NONE', #34062, #11657, #12269 ) ;
#27269=DIRECTION ( 'NONE',  ( 0.000000000000000000, -0.8063205929144885431, 0.5914787413272156735 ) ) ;
#27272=VERTEX_POINT ( 'NONE', #39623 ) ;
#27310=CARTESIAN_POINT ( 'NONE',  ( -0.05464101615137787610, -2.551729310907437043, -0.5086726180052709712 ) ) ;
#27330=EDGE_CURVE ( 'NONE', #25808, #36294, #34258, .T. ) ;
#27333=FACE_OUTER_BOUND ( 'NONE', #19717, .T. ) ;
#27357=EDGE_CURVE ( 'NONE', #32770, #14928, #8550, .T. ) ;
#27490=DIRECTION ( 'NONE',  ( 0.000000000000000000, 0.000000000000000000, 1.000000000000000000 ) ) ;
#27492=ORIENTED_EDGE ( 'NONE', *, *, #662, .T. ) ;
#27511=ADVANCED_FACE ( 'NONE', ( #7227, #19047, #35633, #6479, #31580 ), #9776, .F. ) ;
#27531=VERTEX_POINT ( 'NONE', #25436 ) ;
#27552=EDGE_CURVE ( 'NONE', #36330, #17659, #25818, .T. ) ;
#27554=CARTESIAN_POINT ( 'NONE',  ( -0.02000000000000000042, -1.598492537578166672, -0.3371380022280838773 ) ) ;
#27564=FACE_OUTER_BOUND ( 'NONE', #14654, .T. ) ;
#27568=EDGE_LOOP ( 'NONE', ( #19433, #23179, #24865, #6976 ) ) ;
#27572=CYLINDRICAL_SURFACE ( 'NONE', #39457, 0.07999999999999996003 ) ;
#27576=ORIENTED_EDGE ( 'NONE', *, *, #194, .T. ) ;
#27586=ORIENTED_EDGE ( 'NONE', *, *, #11488, .T. ) ;
#27598=ADVANCED_FACE ( 'NONE', ( #29467 ), #31398, .F. ) ;
#27603=EDGE_CURVE ( 'NONE', #7855, #13458, #32339, .T. ) ;
#27605=CYLINDRICAL_SURFACE ( 'NONE', #24536, 0.07999999999999996003 ) ;
#27611=ADVANCED_FACE ( 'NONE', ( #11956 ), #39587, .F. ) ;
#27634=LINE ( 'NONE', #37091, #26650 ) ;
#27641=CIRCLE ( 'NONE', #17782, 0.1620173459747806799 ) ;
#27659=ORIENTED_EDGE ( 'NONE', *, *, #12228, .F. ) ;
#27748=VECTOR ( 'NONE', #13419, 39.37007874015748854 ) ;
#27774=ORIENTED_EDGE ( 'NONE', *, *, #7666, .F. ) ;
#27775=ADVANCED_FACE ( 'NONE', ( #11567 ), #32947, .F. ) ;
#27790=ORIENTED_EDGE ( 'NONE', *, *, #36827, .F. ) ;
#27804=CARTESIAN_POINT ( 'NONE',  ( -0.02000000000000000042, -2.082394770077036661, -0.4779740388940064144 ) ) ;
#27813=AXIS2_PLACEMENT_3D ( 'NONE', #10867, #23628, #23441 ) ;
#27819=AXIS2_PLACEMENT_3D ( 'NONE', #8920, #2961, #8315 ) ;
#27825=LINE ( 'NONE', #12192, #5977 ) ;
#27826=ORIENTED_EDGE ( 'NONE', *, *, #20755, .T. ) ;
#27832=DIRECTION ( 'NONE',  ( 0.000000000000000000, 0.000000000000000000, -1.000000000000000000 ) ) ;
#27833=CARTESIAN_POINT ( 'NONE',  ( -0.08000000000000000167, -2.196071624283071788, -0.8624000883860228894 ) ) ;
#27857=ADVANCED_FACE ( 'NONE', ( #16075 ), #36338, .F. ) ;
#27885=EDGE_CURVE ( 'NONE', #32770, #37196, #12774, .T. ) ;
#27933=CARTESIAN_POINT ( 'NONE',  ( -0.02000000000000000042, -2.183180860297908144, -0.4937760292030871079 ) ) ;
#27950=EDGE_LOOP ( 'NONE', ( #33017, #17601, #19816, #22726, #3699 ) ) ;
#27954=ORIENTED_EDGE ( 'NONE', *, *, #4642, .F. ) ;
#27976=CARTESIAN_POINT ( 'NONE',  ( -0.02000000000000000042, -2.122347498858831116, -0.8313396097929491857 ) ) ;
#27978=ORIENTED_EDGE ( 'NONE', *, *, #14964, .T. ) ;
#28057=DIRECTION ( 'NONE',  ( -1.000000000000000000, -0.000000000000000000, -0.000000000000000000 ) ) ;
#28077=ORIENTED_EDGE ( 'NONE', *, *, #28522, .F. ) ;
#28091=CARTESIAN_POINT ( 'NONE',  ( -0.05464101615137795936, -1.598492537578166672, -0.1971380022280825872 ) ) ;
#28148=CARTESIAN_POINT ( 'NONE',  ( -0.02000000000000000042, -2.253856486606507836, -0.7252438489935795207 ) ) ;
#28164=CARTESIAN_POINT ( 'NONE',  ( -0.08000000000000000167, -1.659335422034822205, 0.2169804935274543545 ) ) ;
#28216=FACE_OUTER_BOUND ( 'NONE', #21806, .T. ) ;
#28224=EDGE_LOOP ( 'NONE', ( #9205, #25814, #15981, #4040 ) ) ;
#28241=ADVANCED_FACE ( 'NONE', ( #11515 ), #8600, .T. ) ;
#28267=ORIENTED_EDGE ( 'NONE', *, *, #31898, .T. ) ;
#28274=DIRECTION ( 'NONE',  ( 1.000000000000000000, -0.000000000000000000, -0.000000000000000000 ) ) ;
#28279=EDGE_CURVE ( 'NONE', #22522, #21046, #18910, .T. ) ;
#28283=DIRECTION ( 'NONE',  ( -1.000000000000000000, -0.000000000000000000, -0.000000000000000000 ) ) ;
#28323=CARTESIAN_POINT ( 'NONE',  ( -0.02000000000000000042, -2.183180860297908144, -0.4937760292030871079 ) ) ;
#28339=EDGE_CURVE ( 'NONE', #890, #40614, #1541, .T. ) ;
#28344=EDGE_LOOP ( 'NONE', ( #6810, #18215, #4600, #13838, #23192, #33949, #9818, #33699, #36064 ) ) ;
#28367=VECTOR ( 'NONE', #14408, 39.37007874015748143 ) ;
#28391=CARTESIAN_POINT ( 'NONE',  ( -0.02000000000000000042, -2.097192720079996242, -0.6592403319832980113 ) ) ;
#28402=CARTESIAN_POINT ( 'NONE',  ( -0.05464101615137761936, -1.906060000575976243, -0.2916525572568464675 ) ) ;
#28427=ORIENTED_EDGE ( 'NONE', *, *, #699, .F. ) ;
#28430=DIRECTION ( 'NONE',  ( 1.000000000000000000, -0.000000000000000000, -0.000000000000000000 ) ) ;
#28464=DIRECTION ( 'NONE',  ( 1.000000000000000000, 0.000000000000000000, 0.000000000000000000 ) ) ;
#28472=CARTESIAN_POINT ( 'NONE',  ( -0.08000000000000000167, -1.906060000575976021, -0.2916525572568466340 ) ) ;
#28505=CARTESIAN_POINT ( 'NONE',  ( -0.05464101615137767487, -1.737515812098395118, -0.8661170628529262228 ) ) ;
#28509=FACE_OUTER_BOUND ( 'NONE', #15335, .T. ) ;
#28522=EDGE_CURVE ( 'NONE', #11393, #2067, #33694, .T. ) ;
#28554=ORIENTED_EDGE ( 'NONE', *, *, #19742, .F. ) ;
#28561=EDGE_LOOP ( 'NONE', ( #35927, #29078, #9751, #19774 ) ) ;
#28575=DIRECTION ( 'NONE',  ( 0.000000000000000000, -0.3882559824134196313, 0.9215515678030125057 ) ) ;
#28595=ORIENTED_EDGE ( 'NONE', *, *, #26982, .T. ) ;
#28599=EDGE_CURVE ( 'NONE', #12256, #30547, #26291, .T. ) ;
#28602=CARTESIAN_POINT ( 'NONE',  ( -0.02000000000000000042, -1.944084441611813707, -0.4562887203618206655 ) ) ;
#28604=VECTOR ( 'NONE', #3509, 39.37007874015748854 ) ;
#28613=CARTESIAN_POINT ( 'NONE',  ( -0.08000000000000000167, -2.321277022828569958, -0.5785054236952983375 ) ) ;
#28619=CARTESIAN_POINT ( 'NONE',  ( -0.05464101615137786222, -2.183180860297908144, -0.4937760292030871079 ) ) ;
#28624=DIRECTION ( 'NONE',  ( 1.000000000000000000, -0.000000000000000000, -0.000000000000000000 ) ) ;
#28643=VECTOR ( 'NONE', #20892, 39.37007874015748143 ) ;
#28653=EDGE_CURVE ( 'NONE', #27272, #25698, #19705, .T. ) ;
#28681=DIRECTION ( 'NONE',  ( -0.4999999999999972800, -0.7041083277100139703, -0.5042137075183601436 ) ) ;
#28686=VERTEX_POINT ( 'NONE', #18865 ) ;
#28729=DIRECTION ( 'NONE',  ( 1.000000000000000000, 0.000000000000000000, 0.000000000000000000 ) ) ;
#28757=AXIS2_PLACEMENT_3D ( 'NONE', #2684, #22039, #21623 ) ;
#28773=DIRECTION ( 'NONE',  ( -0.4999999999999973910, 0.6535520748299027405, 0.5682162312760273837 ) ) ;
#28785=ORIENTED_EDGE ( 'NONE', *, *, #17728, .F. ) ;
#28789=CARTESIAN_POINT ( 'NONE',  ( -0.05464101615137762630, -1.944084441611813707, -0.4562887203618206655 ) ) ;
#28813=EDGE_CURVE ( 'NONE', #8744, #20771, #283, .T. ) ;
#28844=DIRECTION ( 'NONE',  ( -1.000000000000000000, -0.000000000000000000, -0.000000000000000000 ) ) ;
#28866=EDGE_CURVE ( 'NONE', #12909, #9415, #36511, .T. ) ;
#28881=CARTESIAN_POINT ( 'NONE',  ( -0.02000000000000000042, -1.538828486247671101, 0.2167077994389897955 ) ) ;
#28894=ORIENTED_EDGE ( 'NONE', *, *, #19808, .F. ) ;
#28902=PLANE ( 'NONE',  #4306 ) ;
#28928=ORIENTED_EDGE ( 'NONE', *, *, #23993, .T. ) ;
#28954=DIRECTION ( 'NONE',  ( 0.000000000000000000, 0.000000000000000000, -1.000000000000000000 ) ) ;
#28961=FACE_OUTER_BOUND ( 'NONE', #39915, .T. ) ;
#28964=CARTESIAN_POINT ( 'NONE',  ( -0.02000000000000000042, -1.599201040860868339, 0.1842182323853684411 ) ) ;
#28967=CARTESIAN_POINT ( 'NONE',  ( -0.02000000000000000042, -2.196071624283071788, -0.8624000883860228894 ) ) ;
#28970=AXIS2_PLACEMENT_3D ( 'NONE', #27933, #18260, #30805 ) ;
#28987=CARTESIAN_POINT ( 'NONE',  ( -0.02000000000000000042, -2.071870001606465284, -0.3441689154348898660 ) ) ;
#28989=PLANE ( 'NONE',  #10920 ) ;
#29034=CARTESIAN_POINT ( 'NONE',  ( -0.05464101615137761936, -2.039246558356380135, -0.5681570558249129377 ) ) ;
#29057=CARTESIAN_POINT ( 'NONE',  ( -0.02000000000000000042, -2.070343076906777213, -0.2454056712452573896 ) ) ;
#29066=CARTESIAN_POINT ( 'NONE',  ( -0.08000000000000000167, -1.646519645934556131, -0.1171471737359304072 ) ) ;
#29078=ORIENTED_EDGE ( 'NONE', *, *, #7367, .F. ) ;
#29105=DIRECTION ( 'NONE',  ( 0.000000000000000000, 0.000000000000000000, -1.000000000000000000 ) ) ;
#29107=CARTESIAN_POINT ( 'NONE',  ( -0.02000000000000000042, -1.806850731084499673, -0.8362717670553321270 ) ) ;
#29115=DIRECTION ( 'NONE',  ( 0.000000000000000000, 0.000000000000000000, -1.000000000000000000 ) ) ;
#29116=VERTEX_POINT ( 'NONE', #39539 ) ;
#29157=VECTOR ( 'NONE', #32006, 39.37007874015748143 ) ;
#29168=DIRECTION ( 'NONE',  ( 0.000000000000000000, 0.8063205929144885431, -0.5914787413272156735 ) ) ;
#29181=CYLINDRICAL_SURFACE ( 'NONE', #36372, 0.4488493849861018847 ) ;
#29235=DIRECTION ( 'NONE',  ( 0.000000000000000000, 0.000000000000000000, 1.000000000000000000 ) ) ;
#29256=APPLICATION_CONTEXT ( 'configuration controlled 3d designs of mechanical parts and assemblies' ) ;
#29269=CARTESIAN_POINT ( 'NONE',  ( -0.08000000000000000167, -2.070343076906777213, -0.2454056712452573896 ) ) ;
#29303=CIRCLE ( 'NONE', #22103, 0.6143128707267527799 ) ;
#29324=ADVANCED_FACE ( 'NONE', ( #31275 ), #29797, .F. ) ;
#29337=ADVANCED_FACE ( 'NONE', ( #16044 ), #20620, .F. ) ;
#29363=ORIENTED_EDGE ( 'NONE', *, *, #3164, .T. ) ;
#29364=ORIENTED_EDGE ( 'NONE', *, *, #39589, .F. ) ;
#29395=VERTEX_POINT ( 'NONE', #6969 ) ;
#29398=CARTESIAN_POINT ( 'NONE',  ( -0.02000000000000000042, -2.542046649843399564, -0.2305290188067205537 ) ) ;
#29412=ORIENTED_EDGE ( 'NONE', *, *, #22495, .F. ) ;
#29419=EDGE_CURVE ( 'NONE', #30280, #15898, #19328, .T. ) ;
#29445=VERTEX_POINT ( 'NONE', #16252 ) ;
#29467=FACE_OUTER_BOUND ( 'NONE', #5948, .T. ) ;
#29485=EDGE_CURVE ( 'NONE', #27531, #37987, #40335, .T. ) ;
#29502=CYLINDRICAL_SURFACE ( 'NONE', #397, 0.07999999999999996003 ) ;
#29518=CARTESIAN_POINT ( 'NONE',  ( -0.05464101615137761936, -1.851224977018630868, -0.7958870385335592434 ) ) ;
#29525=DIRECTION ( 'NONE',  ( 0.000000000000000000, -0.8585432690668222122, 0.5127411190260187102 ) ) ;
#29531=ORIENTED_EDGE ( 'NONE', *, *, #3448, .T. ) ;
#29536=FACE_OUTER_BOUND ( 'NONE', #11235, .T. ) ;
#29539=DIRECTION ( 'NONE',  ( 0.000000000000000000, 0.000000000000000000, -1.000000000000000000 ) ) ;
#29558=DIRECTION ( 'NONE',  ( -1.000000000000000000, -0.000000000000000000, -0.000000000000000000 ) ) ;
#29612=ADVANCED_FACE ( 'NONE', ( #40048 ), #30004, .F. ) ;
#29630=DIRECTION ( 'NONE',  ( 0.4999999999999969469, -0.5122356157878158456, -0.6982941170584784363 ) ) ;
#29647=CARTESIAN_POINT ( 'NONE',  ( -0.02000000000000000042, -1.599201040860868339, 0.1642182323853691728 ) ) ;
#29661=VECTOR ( 'NONE', #20800, 39.37007874015748143 ) ;
#29671=CIRCLE ( 'NONE', #3378, 0.08000000000000000167 ) ;
#29673=LINE ( 'NONE', #11573, #14001 ) ;
#29685=AXIS2_PLACEMENT_3D ( 'NONE', #12576, #25137, #22074 ) ;
#29724=CARTESIAN_POINT ( 'NONE',  ( -0.02000000000000000042, -2.049319608666233528, -0.3639547633631710633 ) ) ;
#29732=EDGE_LOOP ( 'NONE', ( #25418, #23065, #4772, #26241 ) ) ;
#29748=FACE_OUTER_BOUND ( 'NONE', #38640, .T. ) ;
#29758=ORIENTED_EDGE ( 'NONE', *, *, #38360, .F. ) ;
#29764=AXIS2_PLACEMENT_3D ( 'NONE', #28619, #22258, #5972 ) ;
#29788=ORIENTED_EDGE ( 'NONE', *, *, #40311, .F. ) ;
#29794=VERTEX_POINT ( 'NONE', #7518 ) ;
#29797=CONICAL_SURFACE ( 'NONE', #10095, 0.1400000000000007350, 1.047197551196601184 ) ;
#29819=CARTESIAN_POINT ( 'NONE',  ( -0.02000000000000000042, -2.070343076906777213, -0.2454056712452573896 ) ) ;
#29820=AXIS2_PLACEMENT_3D ( 'NONE', #18617, #31175, #15540 ) ;
#29875=DIRECTION ( 'NONE',  ( 1.000000000000000000, 0.000000000000000000, 0.000000000000000000 ) ) ;
#29908=ORIENTED_EDGE ( 'NONE', *, *, #10242, .F. ) ;
#29915=ORIENTED_EDGE ( 'NONE', *, *, #16057, .T. ) ;
#29925=CONICAL_SURFACE ( 'NONE', #12179, 0.01999999999999924061, 1.047197551196600962 ) ;
#29927=CONICAL_SURFACE ( 'NONE', #35186, 0.1020173459747799466, 1.047197551196601184 ) ;
#29934=ADVANCED_FACE ( 'NONE', ( #29536 ), #30150, .F. ) ;
#29954=ORIENTED_EDGE ( 'NONE', *, *, #33881, .T. ) ;
#29965=ORIENTED_EDGE ( 'NONE', *, *, #19742, .T. ) ;
#29983=CARTESIAN_POINT ( 'NONE',  ( -0.02000000000000000042, -1.772778095317936620, -0.3120197613628934441 ) ) ;
#30004=CYLINDRICAL_SURFACE ( 'NONE', #12733, 0.08000000000000000167 ) ;
#30023=EDGE_LOOP ( 'NONE', ( #12625, #13416, #5294, #18155 ) ) ;
#30025=EDGE_LOOP ( 'NONE', ( #20900, #29788, #22980, #38248, #37862 ) ) ;
#30032=DIRECTION ( 'NONE',  ( 1.000000000000000000, 0.000000000000000000, 0.000000000000000000 ) ) ;
#30034=EDGE_CURVE ( 'NONE', #21212, #22522, #21330, .T. ) ;
#30048=CARTESIAN_POINT ( 'NONE',  ( -0.02000000000000000042, -1.845925619402022155, -0.3444148183989317880 ) ) ;
#30059=ORIENTED_EDGE ( 'NONE', *, *, #39691, .F. ) ;
#30074=DIRECTION ( 'NONE',  ( 1.000000000000000000, 0.000000000000000000, 0.000000000000000000 ) ) ;
#30083=ADVANCED_FACE ( 'NONE', ( #9755 ), #40359, .F. ) ;
#30106=DIRECTION ( 'NONE',  ( 0.000000000000000000, 0.000000000000000000, -1.000000000000000000 ) ) ;
#30108=EDGE_CURVE ( 'NONE', #23547, #5057, #14079, .T. ) ;
#30134=DIRECTION ( 'NONE',  ( -1.000000000000000000, -0.000000000000000000, -0.000000000000000000 ) ) ;
#30140=CARTESIAN_POINT ( 'NONE',  ( -0.02000000000000000042, -1.584107902207569696, 0.1773406241487738566 ) ) ;
#30150=CYLINDRICAL_SURFACE ( 'NONE', #16033, 0.08000000000000000167 ) ;
#30175=CARTESIAN_POINT ( 'NONE',  ( -0.02000000000000000042, -1.751754812988976395, -0.02481321673728002081 ) ) ;
#30187=DIRECTION ( 'NONE',  ( -1.000000000000000000, -0.000000000000000000, -0.000000000000000000 ) ) ;
#30189=ORIENTED_EDGE ( 'NONE', *, *, #16968, .F. ) ;
#30229=CIRCLE ( 'NONE', #32874, 0.07999999999999996003 ) ;
#30230=DIRECTION ( 'NONE',  ( -0.4999999999999962252, 0.4092454907131379271, -0.7632287522957755810 ) ) ;
#30240=EDGE_CURVE ( 'NONE', #11393, #20672, #8080, .T. ) ;
#30251=FACE_OUTER_BOUND ( 'NONE', #8437, .T. ) ;
#30254=CARTESIAN_POINT ( 'NONE',  ( -0.02000000000000000042, -2.177105168660885326, -0.2518349584362399862 ) ) ;
#30260=DIRECTION ( 'NONE',  ( 0.000000000000000000, 0.000000000000000000, -1.000000000000000000 ) ) ;
#30277=ADVANCED_FACE ( 'NONE', ( #17147 ), #27235, .F. ) ;
#30280=VERTEX_POINT ( 'NONE', #39767 ) ;
#30291=ORIENTED_EDGE ( 'NONE', *, *, #15343, .F. ) ;
#30315=VECTOR ( 'NONE', #8542, 39.37007874015748143 ) ;
#30319=VECTOR ( 'NONE', #29875, 39.37007874015748143 ) ;
#30338=LINE ( 'NONE', #17598, #21361 ) ;
#30345=DIRECTION ( 'NONE',  ( 1.000000000000000000, 0.000000000000000000, 0.000000000000000000 ) ) ;
#30353=DIRECTION ( 'NONE',  ( -1.000000000000000000, -0.000000000000000000, -0.000000000000000000 ) ) ;
#30361=CARTESIAN_POINT ( 'NONE',  ( -0.02000000000000000042, -2.196071624283071788, -0.8624000883860228894 ) ) ;
#30387=EDGE_CURVE ( 'NONE', #7319, #22988, #24617, .T. ) ;
#30404=DIRECTION ( 'NONE',  ( -1.000000000000000000, -0.000000000000000000, -0.000000000000000000 ) ) ;
#30412=ORIENTED_EDGE ( 'NONE', *, *, #2960, .T. ) ;
#30419=EDGE_LOOP ( 'NONE', ( #22850, #12752, #27790, #10318 ) ) ;
#30429=CONICAL_SURFACE ( 'NONE', #16622, 0.1400000000000012623, 1.047197551196601850 ) ;
#30442=CARTESIAN_POINT ( 'NONE',  ( -0.05464101615137796630, -1.750394882718339762, -0.1142373872069606250 ) ) ;
#30449=AXIS2_PLACEMENT_3D ( 'NONE', #25448, #28729, #7092 ) ;
#30456=EDGE_LOOP ( 'NONE', ( #25060, #179, #38011, #28785 ) ) ;
#30471=FACE_OUTER_BOUND ( 'NONE', #15281, .T. ) ;
#30488=AXIS2_PLACEMENT_3D ( 'NONE', #13962, #26533, #39073 ) ;
#30496=DIRECTION ( 'NONE',  ( 0.000000000000000000, 0.000000000000000000, -1.000000000000000000 ) ) ;
#30498=AXIS2_PLACEMENT_3D ( 'NONE', #4395, #35874, #26830 ) ;
#30524=ORIENTED_EDGE ( 'NONE', *, *, #9484, .F. ) ;
#30547=VERTEX_POINT ( 'NONE', #32316 ) ;
#30569=EDGE_CURVE ( 'NONE', #32770, #31436, #12123, .T. ) ;
#30658=VERTEX_POINT ( 'NONE', #16909 ) ;
#30660=ORIENTED_EDGE ( 'NONE', *, *, #31693, .T. ) ;
#30669=ORIENTED_EDGE ( 'NONE', *, *, #3120, .F. ) ;
#30704=ORIENTED_EDGE ( 'NONE', *, *, #34778, .T. ) ;
#30744=ORIENTED_EDGE ( 'NONE', *, *, #10242, .T. ) ;
#30764=ORIENTED_EDGE ( 'NONE', *, *, #14964, .F. ) ;
#30770=DIRECTION ( 'NONE',  ( 0.000000000000000000, 0.000000000000000000, -1.000000000000000000 ) ) ;
#30793=DIRECTION ( 'NONE',  ( 0.000000000000000000, 0.000000000000000000, 1.000000000000000000 ) ) ;
#30796=CARTESIAN_POINT ( 'NONE',  ( -0.05464101615137761936, -1.984114763688379579, -0.7731012124309359912 ) ) ;
#30805=DIRECTION ( 'NONE',  ( 0.000000000000000000, 0.000000000000000000, 1.000000000000000000 ) ) ;
#30814=ORIENTED_EDGE ( 'NONE', *, *, #13186, .T. ) ;
#30846=EDGE_CURVE ( 'NONE', #5340, #5797, #30863, .T. ) ;
#30855=ORIENTED_EDGE ( 'NONE', *, *, #3448, .F. ) ;
#30863=LINE ( 'NONE', #36637, #40393 ) ;
#30891=AXIS2_PLACEMENT_3D ( 'NONE', #38437, #7149, #19716 ) ;
#30893=CARTESIAN_POINT ( 'NONE',  ( -0.02000000000000000042, -1.459219328725982034, -0.1828911325362468643 ) ) ;
#30904=VERTEX_POINT ( 'NONE', #17898 ) ;
#30911=VERTEX_POINT ( 'NONE', #40323 ) ;
#30914=CIRCLE ( 'NONE', #18429, 0.08000000000000000167 ) ;
#30919=ORIENTED_EDGE ( 'NONE', *, *, #17708, .F. ) ;
#30927=CYLINDRICAL_SURFACE ( 'NONE', #8815, 0.08000000000000000167 ) ;
#30950=DIRECTION ( 'NONE',  ( 0.000000000000000000, 0.000000000000000000, -1.000000000000000000 ) ) ;
#30979=FACE_OUTER_BOUND ( 'NONE', #30456, .T. ) ;
#30990=CARTESIAN_POINT ( 'NONE',  ( -0.02000000000000000042, -1.659335422034822205, 0.2169804935274543545 ) ) ;
#31027=EDGE_CURVE ( 'NONE', #17786, #3745, #5557, .T. ) ;
#31028=CARTESIAN_POINT ( 'NONE',  ( -0.02000000000000000042, -2.092549851682985018, -0.5406114768595331466 ) ) ;
#31037=AXIS2_PLACEMENT_3D ( 'NONE', #25283, #443, #3258 ) ;
#31047=CARTESIAN_POINT ( 'NONE',  ( -0.05464101615137786222, -2.196071624283071788, -0.9424000883860228495 ) ) ;
#31056=LINE ( 'NONE', #9233, #35476 ) ;
#31058=CARTESIAN_POINT ( 'NONE',  ( -0.08000000000000000167, -2.589364949149576933, -0.2950346662398796171 ) ) ;
#31060=AXIS2_PLACEMENT_3D ( 'NONE', #37968, #32544, #22914 ) ;
#31062=CARTESIAN_POINT ( 'NONE',  ( -0.02000000000000000042, -2.320036485105098301, -0.4341690811493933433 ) ) ;
#31067=EDGE_LOOP ( 'NONE', ( #21082, #25525, #3975, #37464 ) ) ;
#31086=EDGE_CURVE ( 'NONE', #34947, #30911, #55, .T. ) ;
#31100=CIRCLE ( 'NONE', #8089, 0.1620173459747806799 ) ;
#31115=ORIENTED_EDGE ( 'NONE', *, *, #24783, .F. ) ;
#31138=ADVANCED_FACE ( 'NONE', ( #36730 ), #8855, .F. ) ;
#31156=ADVANCED_FACE ( 'NONE', ( #29748 ), #2320, .F. ) ;
#31168=AXIS2_PLACEMENT_3D ( 'NONE', #3266, #38631, #19529 ) ;
#31175=DIRECTION ( 'NONE',  ( -1.000000000000000000, -0.000000000000000000, -0.000000000000000000 ) ) ;
#31179=EDGE_LOOP ( 'NONE', ( #31962, #39654, #7830, #13355 ) ) ;
#31184=CYLINDRICAL_SURFACE ( 'NONE', #17148, 0.08000000000000000167 ) ;
#31195=CARTESIAN_POINT ( 'NONE',  ( -0.08000000000000000167, -1.910390638264138685, -0.7420407338378623985 ) ) ;
#31230=DIRECTION ( 'NONE',  ( 0.000000000000000000, 0.000000000000000000, 1.000000000000000000 ) ) ;
#31274=DIRECTION ( 'NONE',  ( 0.000000000000000000, -2.048885995248197236E-14, -1.000000000000000000 ) ) ;
#31275=FACE_OUTER_BOUND ( 'NONE', #15064, .T. ) ;
#31280=CIRCLE ( 'NONE', #6943, 0.07999999999999996003 ) ;
#31300=CARTESIAN_POINT ( 'NONE',  ( -0.08000000000000000167, -2.548345659627495596, -0.2263512047145338768 ) ) ;
#31326=EDGE_CURVE ( 'NONE', #19134, #30280, #14932, .T. ) ;
#31345=DIRECTION ( 'NONE',  ( 0.000000000000000000, 0.000000000000000000, -1.000000000000000000 ) ) ;
#31377=EDGE_CURVE ( 'NONE', #7253, #8899, #37337, .T. ) ;
#31398=CYLINDRICAL_SURFACE ( 'NONE', #8699, 0.07999999999999996003 ) ;
#31436=VERTEX_POINT ( 'NONE', #19036 ) ;
#31451=CARTESIAN_POINT ( 'NONE',  ( -0.02000000000000000042, -1.599201040860868339, 0.2442182323853691606 ) ) ;
#31457=ORIENTED_EDGE ( 'NONE', *, *, #27603, .F. ) ;
#31465=ORIENTED_EDGE ( 'NONE', *, *, #9484, .T. ) ;
#31527=ADVANCED_FACE ( 'NONE', ( #34856 ), #29502, .F. ) ;
#31535=EDGE_CURVE ( 'NONE', #11782, #31436, #34197, .T. ) ;
#31542=EDGE_CURVE ( 'NONE', #22988, #10878, #27634, .T. ) ;
#31580=FACE_BOUND ( 'NONE', #21471, .T. ) ;
#31583=AXIS2_PLACEMENT_3D ( 'NONE', #36525, #25195, #557 ) ;
#31585=DIRECTION ( 'NONE',  ( 0.000000000000000000, -0.5914787413272157846, -0.8063205929144887651 ) ) ;
#31629=ORIENTED_EDGE ( 'NONE', *, *, #7210, .T. ) ;
#31646=DIRECTION ( 'NONE',  ( -0.000000000000000000, -0.6595282642760668113, -0.7516797646744247663 ) ) ;
#31664=EDGE_LOOP ( 'NONE', ( #8444, #26920, #21321, #11819 ) ) ;
#31675=VERTEX_POINT ( 'NONE', #26183 ) ;
#31693=EDGE_CURVE ( 'NONE', #8526, #34885, #4094, .T. ) ;
#31704=AXIS2_PLACEMENT_3D ( 'NONE', #26388, #10962, #3200 ) ;
#31706=LINE ( 'NONE', #16290, #22838 ) ;
#31764=EDGE_CURVE ( 'NONE', #30658, #25698, #6992, .T. ) ;
#31778=ORIENTED_EDGE ( 'NONE', *, *, #10692, .F. ) ;
#31803=DIRECTION ( 'NONE',  ( 0.000000000000000000, 0.000000000000000000, 1.000000000000000000 ) ) ;
#31812=CARTESIAN_POINT ( 'NONE',  ( -0.02000000000000000042, -2.268861055605315258, -0.3290426542847164626 ) ) ;
#31827=EDGE_LOOP ( 'NONE', ( #38501, #14617, #9624, #7633 ) ) ;
#31830=ADVANCED_FACE ( 'NONE', ( #39075 ), #26537, .F. ) ;
#31858=DIRECTION ( 'NONE',  ( -1.000000000000000000, -0.000000000000000000, -0.000000000000000000 ) ) ;
#31859=CONICAL_SURFACE ( 'NONE', #35151, 0.4488493849861018292, 1.047197551196600962 ) ;
#31862=CARTESIAN_POINT ( 'NONE',  ( -0.02000000000000000042, -1.802948570736253586, -0.8420585814095631338 ) ) ;
#31885=FACE_OUTER_BOUND ( 'NONE', #39541, .T. ) ;
#31892=ORIENTED_EDGE ( 'NONE', *, *, #18590, .T. ) ;
#31898=EDGE_CURVE ( 'NONE', #12543, #5617, #17473, .T. ) ;
#31904=ADVANCED_FACE ( 'NONE', ( #23860 ), #29925, .T. ) ;
#31910=DIRECTION ( 'NONE',  ( 1.000000000000000000, 0.000000000000000000, 0.000000000000000000 ) ) ;
#31921=DIRECTION ( 'NONE',  ( -1.000000000000000000, -0.000000000000000000, -0.000000000000000000 ) ) ;
#31962=ORIENTED_EDGE ( 'NONE', *, *, #19290, .F. ) ;
#31989=CARTESIAN_POINT ( 'NONE',  ( -0.05464101615137785528, -2.196538720661423749, -0.6552417777791260667 ) ) ;
#31991=ORIENTED_EDGE ( 'NONE', *, *, #13433, .F. ) ;
#32006=DIRECTION ( 'NONE',  ( -1.000000000000000000, -0.000000000000000000, -0.000000000000000000 ) ) ;
#32010=CARTESIAN_POINT ( 'NONE',  ( -0.05464101615137773038, -2.626773565144302935, -0.2726934094652516127 ) ) ;
#32017=CARTESIAN_POINT ( 'NONE',  ( -0.08000000000000000167, -2.320036485105098301, -0.2941690811493925528 ) ) ;
#32021=DIRECTION ( 'NONE',  ( 1.000000000000000000, 0.000000000000000000, 0.000000000000000000 ) ) ;
#32047=EDGE_CURVE ( 'NONE', #27531, #16107, #20971, .T. ) ;
#32053=LINE ( 'NONE', #31451, #36277 ) ;
#32059=ADVANCED_FACE ( 'NONE', ( #15399 ), #7869, .F. ) ;
#32067=ORIENTED_EDGE ( 'NONE', *, *, #1882, .F. ) ;
#32076=CARTESIAN_POINT ( 'NONE',  ( -0.02000000000000000042, -2.230494317742474308, -0.6487310457122437146 ) ) ;
#32079=ORIENTED_EDGE ( 'NONE', *, *, #31542, .T. ) ;
#32085=DIRECTION ( 'NONE',  ( 0.3981087504120420228, -0.9173382270707802766, 0.000000000000000000 ) ) ;
#32101=FACE_OUTER_BOUND ( 'NONE', #8178, .T. ) ;
#32109=DIRECTION ( 'NONE',  ( 0.000000000000000000, 0.000000000000000000, -1.000000000000000000 ) ) ;
#32116=EDGE_LOOP ( 'NONE', ( #25863, #30744, #25186, #15835 ) ) ;
#32123=EDGE_CURVE ( 'NONE', #5617, #2236, #38191, .T. ) ;
#32147=EDGE_CURVE ( 'NONE', #2067, #25764, #21392, .T. ) ;
#32150=EDGE_CURVE ( 'NONE', #37816, #40536, #11814, .T. ) ;
#32166=ORIENTED_EDGE ( 'NONE', *, *, #32147, .T. ) ;
#32220=ORIENTED_EDGE ( 'NONE', *, *, #36145, .T. ) ;
#32245=DIRECTION ( 'NONE',  ( 1.000000000000000000, -0.000000000000000000, -0.000000000000000000 ) ) ;
#32247=ORIENTED_EDGE ( 'NONE', *, *, #22464, .F. ) ;
#32262=ORIENTED_EDGE ( 'NONE', *, *, #13793, .T. ) ;
#32273=AXIS2_PLACEMENT_3D ( 'NONE', #28148, #13105, #25665 ) ;
#32301=ORIENTED_EDGE ( 'NONE', *, *, #30569, .T. ) ;
#32304=DIRECTION ( 'NONE',  ( 0.000000000000000000, 0.000000000000000000, -1.000000000000000000 ) ) ;
#32305=CIRCLE ( 'NONE', #37561, 0.08000000000000000167 ) ;
#32316=CARTESIAN_POINT ( 'NONE',  ( -0.05464101615137771650, -1.538828486247671101, 0.2167077994389897955 ) ) ;
#32327=ORIENTED_EDGE ( 'NONE', *, *, #9195, .F. ) ;
#32329=DIRECTION ( 'NONE',  ( 0.000000000000000000, 0.000000000000000000, -1.000000000000000000 ) ) ;
#32339=CIRCLE ( 'NONE', #31704, 0.5756329413417604624 ) ;
#32340=FACE_OUTER_BOUND ( 'NONE', #8237, .T. ) ;
#32349=CONICAL_SURFACE ( 'NONE', #8714, 0.01999999999999927530, 1.047197551196600962 ) ;
#32357=VERTEX_POINT ( 'NONE', #34138 ) ;
#32401=CIRCLE ( 'NONE', #16652, 0.1620173459747806799 ) ;
#32406=DIRECTION ( 'NONE',  ( 0.000000000000000000, 1.951319995474454795E-15, -1.000000000000000000 ) ) ;
#32440=FACE_OUTER_BOUND ( 'NONE', #31067, .T. ) ;
#32457=FACE_OUTER_BOUND ( 'NONE', #40196, .T. ) ;
#32470=CARTESIAN_POINT ( 'NONE',  ( -0.05464101615137762630, -1.910390638264138685, -0.7420407338378623985 ) ) ;
#32471=ORIENTED_EDGE ( 'NONE', *, *, #40125, .F. ) ;
#32509=EDGE_CURVE ( 'NONE', #14209, #4083, #3092, .T. ) ;
#32510=ORIENTED_EDGE ( 'NONE', *, *, #216, .T. ) ;
#32522=AXIS2_PLACEMENT_3D ( 'NONE', #25402, #22926, #13233 ) ;
#32544=DIRECTION ( 'NONE',  ( -1.000000000000000000, -0.000000000000000000, -0.000000000000000000 ) ) ;
#32552=CARTESIAN_POINT ( 'NONE',  ( -0.05464101615137763324, -2.183180860297908144, -0.4937760292030871079 ) ) ;
#32561=DIRECTION ( 'NONE',  ( 0.000000000000000000, 0.000000000000000000, -1.000000000000000000 ) ) ;
#32643=ORIENTED_EDGE ( 'NONE', *, *, #32509, .T. ) ;
#32653=CARTESIAN_POINT ( 'NONE',  ( -0.05464101615137770263, -2.183180860297908144, -0.3317586832283064280 ) ) ;
#32655=CARTESIAN_POINT ( 'NONE',  ( -0.05464101615137768181, -2.367354784411275670, -0.3586747285825516718 ) ) ;
#32658=ADVANCED_FACE ( 'NONE', ( #6049 ), #22695, .F. ) ;
#32662=EDGE_CURVE ( 'NONE', #10881, #6598, #11428, .T. ) ;
#32690=CYLINDRICAL_SURFACE ( 'NONE', #26706, 0.5756329413417603513 ) ;
#32709=DIRECTION ( 'NONE',  ( 1.000000000000000000, 0.000000000000000000, 0.000000000000000000 ) ) ;
#32731=EDGE_LOOP ( 'NONE', ( #22681, #28427, #21808, #5388 ) ) ;
#32732=ORIENTED_EDGE ( 'NONE', *, *, #8003, .T. ) ;
#32770=VERTEX_POINT ( 'NONE', #1104 ) ;
#32812=DIRECTION ( 'NONE',  ( -1.000000000000000000, -0.000000000000000000, -0.000000000000000000 ) ) ;
#32829=ORIENTED_EDGE ( 'NONE', *, *, #1662, .T. ) ;
#32831=ADVANCED_FACE ( 'NONE', ( #1122 ), #4365, .F. ) ;
#32849=EDGE_CURVE ( 'NONE', #34885, #37816, #10107, .T. ) ;
#32853=LINE ( 'NONE', #4656, #6123 ) ;
#32860=ORIENTED_EDGE ( 'NONE', *, *, #30240, .F. ) ;
#32874=AXIS2_PLACEMENT_3D ( 'NONE', #19767, #38688, #32304 ) ;
#32908=CARTESIAN_POINT ( 'NONE',  ( -0.02000000000000000042, -2.183180860297908144, -0.3317586832283064280 ) ) ;
#32929=ADVANCED_FACE ( 'NONE', ( #21022 ), #20637, .T. ) ;
#32940=DIRECTION ( 'NONE',  ( 1.000000000000000000, 0.000000000000000000, 0.000000000000000000 ) ) ;
#32947=PLANE ( 'NONE',  #883 ) ;
#32959=CARTESIAN_POINT ( 'NONE',  ( -0.02000000000000000042, -2.179113517810423062, -0.3318097452986852880 ) ) ;
#32975=CARTESIAN_POINT ( 'NONE',  ( -0.02000000000000000042, -2.196071624283071788, -1.002400088386023791 ) ) ;
#32980=FACE_OUTER_BOUND ( 'NONE', #31179, .T. ) ;
#32992=AXIS2_PLACEMENT_3D ( 'NONE', #34425, #22504, #40596 ) ;
#32999=CARTESIAN_POINT ( 'NONE',  ( -0.02000000000000000042, -1.614234636154356251, 0.1774087976708900172 ) ) ;
#33017=ORIENTED_EDGE ( 'NONE', *, *, #31377, .F. ) ;
#33028=CARTESIAN_POINT ( 'NONE',  ( -0.05464101615137762630, -1.968175500587574067, -0.6048844944454191408 ) ) ;
#33061=CARTESIAN_POINT ( 'NONE',  ( -0.02000000000000000042, -1.761115123485013534, -0.1975702831323159492 ) ) ;
#33095=AXIS2_PLACEMENT_3D ( 'NONE', #18303, #15419, #37416 ) ;
#33097=CARTESIAN_POINT ( 'NONE',  ( -0.02000000000000000042, -2.616518742763782601, -0.2555225440839158924 ) ) ;
#33098=AXIS2_PLACEMENT_3D ( 'NONE', #39735, #8655, #11568 ) ;
#33108=AXIS2_PLACEMENT_3D ( 'NONE', #28789, #4075, #26309 ) ;
#33112=VECTOR ( 'NONE', #28681, 39.37007874015748143 ) ;
#33144=ORIENTED_EDGE ( 'NONE', *, *, #3735, .F. ) ;
#33184=ORIENTED_EDGE ( 'NONE', *, *, #38566, .F. ) ;
#33191=ORIENTED_EDGE ( 'NONE', *, *, #18179, .F. ) ;
#33206=VECTOR ( 'NONE', #2542, 39.37007874015748854 ) ;
#33218=CARTESIAN_POINT ( 'NONE',  ( -0.02000000000000000042, -1.910390638264138685, -0.8820407338378629669 ) ) ;
#33221=ORIENTED_EDGE ( 'NONE', *, *, #20111, .T. ) ;
#33228=CLOSED_SHELL ( 'NONE', ( #538, #719, #29324, #39397, #31904, #31138, #21746, #16682, #25865, #27109, #23874, #32831, #16300, #32658, #2208, #18756, #27511, #4882, #24736, #16838, #4410, #5092, #23582, #2452, #11542, #12677, #40353, #36184, #5332, #31830, #5869, #22, #10690, #8623, #4097, #31527, #21582, #11195, #29934, #29612, #38672, #27598, #34111, #6404, #33760, #7951, #404, #7187, #15879, #11827, #30277, #22084, #32059, #24830, #40588, #39062, #20734, #31156, #27775, #29337, #37066, #3391, #24492, #6938, #5189, #5212, #27857, #35127, #10955, #23753, #26032, #27611, #12787, #9424, #32929, #37868, #15804, #20838, #28241, #40171, #15929, #12754, #16440, #30083, #12674, #26042 ) ) ;
#33231=ORIENTED_EDGE ( 'NONE', *, *, #30108, .F. ) ;
#33239=DIRECTION ( 'NONE',  ( 0.000000000000000000, 0.000000000000000000, -1.000000000000000000 ) ) ;
#33258=DIRECTION ( 'NONE',  ( 0.000000000000000000, -0.5914787413272157846, -0.8063205929144887651 ) ) ;
#33295=ORIENTED_EDGE ( 'NONE', *, *, #20966, .T. ) ;
#33324=LINE ( 'NONE', #5130, #25667 ) ;
#33342=DIRECTION ( 'NONE',  ( 0.000000000000000000, 0.000000000000000000, 1.000000000000000000 ) ) ;
#33369=EDGE_CURVE ( 'NONE', #26070, #5313, #35097, .T. ) ;
#33372=ADVANCED_BREP_SHAPE_REPRESENTATION ( '', ( #19265, #27819 ), #3510 ) ;
#33400=ORIENTED_EDGE ( 'NONE', *, *, #27552, .T. ) ;
#33406=LINE ( 'NONE', #37103, #2851 ) ;
#33449=DIRECTION ( 'NONE',  ( 0.000000000000000000, 0.000000000000000000, -1.000000000000000000 ) ) ;
#33465=DIRECTION ( 'NONE',  ( 0.000000000000000000, 0.000000000000000000, -1.000000000000000000 ) ) ;
#33474=CARTESIAN_POINT ( 'NONE',  ( -0.02000000000000000042, -2.196071624283071788, -1.002400088386023791 ) ) ;
#33509=VERTEX_POINT ( 'NONE', #24269 ) ;
#33584=DIRECTION ( 'NONE',  ( 0.000000000000000000, 0.000000000000000000, 1.000000000000000000 ) ) ;
#33596=DIRECTION ( 'NONE',  ( 0.000000000000000000, 0.000000000000000000, -1.000000000000000000 ) ) ;
#33635=CARTESIAN_POINT ( 'NONE',  ( -0.02000000000000000042, -2.049319608666233528, -0.3639547633631710633 ) ) ;
#33640=CARTESIAN_POINT ( 'NONE',  ( -0.08000000000000000167, -1.598492537578166672, -0.1971380022280825872 ) ) ;
#33645=VERTEX_POINT ( 'NONE', #5628 ) ;
#33651=CARTESIAN_POINT ( 'NONE',  ( -0.05464101615137766793, -2.548345659627495596, -0.2263512047145338768 ) ) ;
#33663=DIRECTION ( 'NONE',  ( -1.000000000000000000, -0.000000000000000000, -0.000000000000000000 ) ) ;
#33680=DIRECTION ( 'NONE',  ( -1.000000000000000000, -0.000000000000000000, -0.000000000000000000 ) ) ;
#33685=EDGE_LOOP ( 'NONE', ( #23496, #3289, #2336, #38035, #20103 ) ) ;
#33694=CIRCLE ( 'NONE', #36987, 0.07999999999999996003 ) ;
#33699=ORIENTED_EDGE ( 'NONE', *, *, #23807, .T. ) ;
#33721=CARTESIAN_POINT ( 'NONE',  ( -0.02000000000000000042, -2.180619779672576364, -0.3917908354455199582 ) ) ;
#33742=FACE_OUTER_BOUND ( 'NONE', #34009, .T. ) ;
#33760=ADVANCED_FACE ( 'NONE', ( #24963 ), #30927, .F. ) ;
#33763=DIRECTION ( 'NONE',  ( 1.000000000000000000, -0.000000000000000000, -0.000000000000000000 ) ) ;
#33765=AXIS2_PLACEMENT_3D ( 'NONE', #37189, #3046, #12482 ) ;
#33838=EDGE_CURVE ( 'NONE', #11782, #37196, #10790, .T. ) ;
#33847=EDGE_LOOP ( 'NONE', ( #22524, #38016, #13396, #14882 ) ) ;
#33857=AXIS2_PLACEMENT_3D ( 'NONE', #26486, #33258, #5068 ) ;
#33859=PLANE ( 'NONE',  #39503 ) ;
#33872=CARTESIAN_POINT ( 'NONE',  ( -0.08000000000000000167, -2.253856486606507836, -0.7252438489935795207 ) ) ;
#33881=EDGE_CURVE ( 'NONE', #3745, #8808, #29673, .T. ) ;
#33901=EDGE_CURVE ( 'NONE', #16266, #2769, #12680, .T. ) ;
#33912=ORIENTED_EDGE ( 'NONE', *, *, #11800, .F. ) ;
#33934=EDGE_CURVE ( 'NONE', #40614, #5313, #23327, .T. ) ;
#33945=LINE ( 'NONE', #34332, #12717 ) ;
#33949=ORIENTED_EDGE ( 'NONE', *, *, #11773, .T. ) ;
#33955=DIRECTION ( 'NONE',  ( 0.4999999999999968359, 0.000000000000000000, -0.8660254037844405950 ) ) ;
#33968=DIRECTION ( 'NONE',  ( -1.000000000000000000, 0.000000000000000000, 0.000000000000000000 ) ) ;
#33976=CARTESIAN_POINT ( 'NONE',  ( -0.05464101615137786222, -2.321277022828569958, -0.5785054236952983375 ) ) ;
#33994=ORIENTED_EDGE ( 'NONE', *, *, #40311, .T. ) ;
#34009=EDGE_LOOP ( 'NONE', ( #31778, #32829, #696, #20561 ) ) ;
#34025=EDGE_CURVE ( 'NONE', #38792, #890, #6778, .T. ) ;
#34053=DIRECTION ( 'NONE',  ( -1.000000000000000000, -0.000000000000000000, -0.000000000000000000 ) ) ;
#34062=CARTESIAN_POINT ( 'NONE',  ( -0.05464101615137786222, -2.379949255320110257, -0.6346823614705312533 ) ) ;
#34104=ORIENTED_EDGE ( 'NONE', *, *, #8697, .F. ) ;
#34111=ADVANCED_FACE ( 'NONE', ( #15251 ), #27605, .F. ) ;
#34134=ORIENTED_EDGE ( 'NONE', *, *, #31764, .F. ) ;
#34138=CARTESIAN_POINT ( 'NONE',  ( -0.02000000000000000042, -2.183180860297908144, -0.5562760292030870524 ) ) ;
#34197=LINE ( 'NONE', #24559, #33206 ) ;
#34205=CARTESIAN_POINT ( 'NONE',  ( -0.02000000000000000042, -2.183180860297908144, -0.4937760292030871079 ) ) ;
#34243=VERTEX_POINT ( 'NONE', #9485 ) ;
#34252=AXIS2_PLACEMENT_3D ( 'NONE', #39507, #23696, #15039 ) ;
#34258=LINE ( 'NONE', #33651, #38246 ) ;
#34260=AXIS2_PLACEMENT_3D ( 'NONE', #35306, #16580, #7291 ) ;
#34264=EDGE_CURVE ( 'NONE', #4481, #30904, #15980, .T. ) ;
#34284=DIRECTION ( 'NONE',  ( 0.4999999999999963918, 0.000000000000000000, -0.8660254037844405950 ) ) ;
#34315=DIRECTION ( 'NONE',  ( 0.4441145778363653207, 0.000000000000000000, -0.8959700004761470549 ) ) ;
#34319=CIRCLE ( 'NONE', #32992, 0.7043128707267513056 ) ;
#34332=CARTESIAN_POINT ( 'NONE',  ( -0.07999999999999998779, -2.004218822785767795, -0.4035264592197354561 ) ) ;
#34343=DIRECTION ( 'NONE',  ( -0.4999999999999970024, 0.000000000000000000, 0.8660254037844403729 ) ) ;
#34355=VECTOR ( 'NONE', #32709, 39.37007874015748143 ) ;
#34425=CARTESIAN_POINT ( 'NONE',  ( -0.05464101615137769569, -2.070343076906777213, -0.2454056712452573896 ) ) ;
#34429=CARTESIAN_POINT ( 'NONE',  ( -0.08000000000000000167, -2.058305985490972212, -0.5970033804171128722 ) ) ;
#34431=VECTOR ( 'NONE', #782, 39.37007874015748143 ) ;
#34440=AXIS2_PLACEMENT_3D ( 'NONE', #4796, #20673, #14280 ) ;
#34447=DIRECTION ( 'NONE',  ( 0.000000000000000000, 0.000000000000000000, -1.000000000000000000 ) ) ;
#34471=VECTOR ( 'NONE', #9141, 39.37007874015747433 ) ;
#34507=CIRCLE ( 'NONE', #13518, 0.1400000000000010403 ) ;
#34539=AXIS2_PLACEMENT_3D ( 'NONE', #39429, #11665, #23820 ) ;
#34549=ORIENTED_EDGE ( 'NONE', *, *, #36389, .F. ) ;
#34550=CARTESIAN_POINT ( 'NONE',  ( -0.02000000000000000042, -2.253856486606507836, -0.7252438489935795207 ) ) ;
#34554=ORIENTED_EDGE ( 'NONE', *, *, #26622, .F. ) ;
#34555=AXIS2_PLACEMENT_3D ( 'NONE', #36531, #30353, #26873 ) ;
#34558=VERTEX_POINT ( 'NONE', #26496 ) ;
#34632=FACE_OUTER_BOUND ( 'NONE', #16005, .T. ) ;
#34641=ORIENTED_EDGE ( 'NONE', *, *, #23528, .T. ) ;
#34657=ORIENTED_EDGE ( 'NONE', *, *, #11247, .T. ) ;
#34667=LINE ( 'NONE', #40630, #19832 ) ;
#34686=EDGE_LOOP ( 'NONE', ( #29364, #24772, #17015, #13683 ) ) ;
#34713=ORIENTED_EDGE ( 'NONE', *, *, #6638, .F. ) ;
#34729=PLANE ( 'NONE',  #31037 ) ;
#34760=ORIENTED_EDGE ( 'NONE', *, *, #9195, .T. ) ;
#34769=CARTESIAN_POINT ( 'NONE',  ( -0.05464101615137796630, -1.706654027108509997, -0.06438491259384494791 ) ) ;
#34771=LINE ( 'NONE', #27804, #7404 ) ;
#34778=EDGE_CURVE ( 'NONE', #2236, #12860, #4164, .T. ) ;
#34802=ORIENTED_EDGE ( 'NONE', *, *, #12228, .T. ) ;
#34837=ORIENTED_EDGE ( 'NONE', *, *, #19290, .T. ) ;
#34839=CARTESIAN_POINT ( 'NONE',  ( -0.05464101615137784834, -2.230494317742474308, -0.6487310457122437146 ) ) ;
#34855=ORIENTED_EDGE ( 'NONE', *, *, #6279, .T. ) ;
#34856=FACE_OUTER_BOUND ( 'NONE', #34686, .T. ) ;
#34860=LINE ( 'NONE', #31989, #16546 ) ;
#34867=CIRCLE ( 'NONE', #17134, 0.4488493849861018292 ) ;
#34874=CYLINDRICAL_SURFACE ( 'NONE', #16176, 0.07999999999999996003 ) ;
#34885=VERTEX_POINT ( 'NONE', #5027 ) ;
#34886=CARTESIAN_POINT ( 'NONE',  ( -0.08000000000000000167, -2.070343076906777213, -0.2454056712452573896 ) ) ;
#34944=AXIS2_PLACEMENT_3D ( 'NONE', #38686, #3920, #293 ) ;
#34946=DIRECTION ( 'NONE',  ( 0.000000000000000000, 0.000000000000000000, 1.000000000000000000 ) ) ;
#34947=VERTEX_POINT ( 'NONE', #16088 ) ;
#34950=EDGE_LOOP ( 'NONE', ( #16038, #25057, #17684, #19035 ) ) ;
#34992=VECTOR ( 'NONE', #29630, 39.37007874015748854 ) ;
#34995=ORIENTED_EDGE ( 'NONE', *, *, #17301, .F. ) ;
#35025=( CONVERSION_BASED_UNIT ( 'INCH', #22301 ) LENGTH_UNIT ( ) NAMED_UNIT ( #38313 ) );
#35029=VECTOR ( 'NONE', #20229, 39.37007874015748143 ) ;
#35049=AXIS2_PLACEMENT_3D ( 'NONE', #4282, #16849, #39040 ) ;
#35071=DIRECTION ( 'NONE',  ( -1.000000000000000000, -0.000000000000000000, -0.000000000000000000 ) ) ;
#35096=CARTESIAN_POINT ( 'NONE',  ( -0.02000000000000000042, -2.626773565144302935, -0.1926934094652516249 ) ) ;
#35097=CIRCLE ( 'NONE', #17365, 0.07999999999999996003 ) ;
#35115=CIRCLE ( 'NONE', #27258, 0.07999999999999996003 ) ;
#35127=ADVANCED_FACE ( 'NONE', ( #27564 ), #8776, .F. ) ;
#35129=LINE ( 'NONE', #35332, #7663 ) ;
#35132=ORIENTED_EDGE ( 'NONE', *, *, #27357, .T. ) ;
#35133=AXIS2_PLACEMENT_3D ( 'NONE', #26430, #38967, #23369 ) ;
#35137=CYLINDRICAL_SURFACE ( 'NONE', #19842, 0.08000000000000000167 ) ;
#35143=EDGE_CURVE ( 'NONE', #15479, #11782, #19311, .T. ) ;
#35151=AXIS2_PLACEMENT_3D ( 'NONE', #21069, #39978, #33596 ) ;
#35182=EDGE_CURVE ( 'NONE', #30280, #13990, #33945, .T. ) ;
#35186=AXIS2_PLACEMENT_3D ( 'NONE', #37740, #23298, #22139 ) ;
#35189=DIRECTION ( 'NONE',  ( 1.000000000000000000, -0.000000000000000000, -0.000000000000000000 ) ) ;
#35225=EDGE_LOOP ( 'NONE', ( #34554, #40470, #35369, #5836 ) ) ;
#35227=DIRECTION ( 'NONE',  ( 1.000000000000000000, -0.000000000000000000, -0.000000000000000000 ) ) ;
#35260=AXIS2_PLACEMENT_3D ( 'NONE', #24142, #39748, #36663 ) ;
#35265=LINE ( 'NONE', #28881, #17873 ) ;
#35269=DIRECTION ( 'NONE',  ( 0.000000000000000000, 0.000000000000000000, -1.000000000000000000 ) ) ;
#35302=VERTEX_POINT ( 'NONE', #33721 ) ;
#35306=CARTESIAN_POINT ( 'NONE',  ( -0.02000000000000000042, -2.183180860297908144, -0.4937760292030871079 ) ) ;
#35317=CARTESIAN_POINT ( 'NONE',  ( -0.05464101615137786222, -2.198867511061768809, -0.9423512173156428640 ) ) ;
#35332=CARTESIAN_POINT ( 'NONE',  ( -0.02000000000000000042, -1.737515812098395118, -0.8661170628529262228 ) ) ;
#35335=EDGE_LOOP ( 'NONE', ( #6278, #29965, #13646, #39779 ) ) ;
#35347=CARTESIAN_POINT ( 'NONE',  ( -0.02000000000000000042, -1.584107902207569696, 0.1773406241487738566 ) ) ;
#35356=EDGE_CURVE ( 'NONE', #26267, #38006, #16686, .T. ) ;
#35357=CARTESIAN_POINT ( 'NONE',  ( -0.05464101615137770263, -2.183180860297908144, -0.4937760292030871079 ) ) ;
#35369=ORIENTED_EDGE ( 'NONE', *, *, #38667, .F. ) ;
#35377=DIRECTION ( 'NONE',  ( 1.000000000000000000, -0.000000000000000000, -0.000000000000000000 ) ) ;
#35415=DIRECTION ( 'NONE',  ( 0.000000000000000000, 0.000000000000000000, -1.000000000000000000 ) ) ;
#35433=PLANE ( 'NONE',  #15509 ) ;
#35476=VECTOR ( 'NONE', #15428, 39.37007874015748143 ) ;
#35479=ORIENTED_EDGE ( 'NONE', *, *, #12011, .F. ) ;
#35536=PRODUCT_DEFINITION ( 'UNKNOWN', '', #37152, #38872 ) ;
#35540=AXIS2_PLACEMENT_3D ( 'NONE', #6923, #12693, #25254 ) ;
#35603=VECTOR ( 'NONE', #17664, 39.37007874015748854 ) ;
#35611=ORIENTED_EDGE ( 'NONE', *, *, #35783, .F. ) ;
#35614=DIRECTION ( 'NONE',  ( 1.000000000000000000, 0.000000000000000000, 0.000000000000000000 ) ) ;
#35633=FACE_OUTER_BOUND ( 'NONE', #36753, .T. ) ;
#35652=AXIS2_PLACEMENT_3D ( 'NONE', #9164, #18027, #9365 ) ;
#35666=AXIS2_PLACEMENT_3D ( 'NONE', #9423, #9033, #15403 ) ;
#35686=AXIS2_PLACEMENT_3D ( 'NONE', #39332, #10754, #36046 ) ;
#35699=CIRCLE ( 'NONE', #27813, 0.1400000000000005684 ) ;
#35723=EDGE_LOOP ( 'NONE', ( #11164, #26326, #14561, #14279 ) ) ;
#35726=LINE ( 'NONE', #1207, #20840 ) ;
#35773=AXIS2_PLACEMENT_3D ( 'NONE', #16082, #28624, #494 ) ;
#35777=CARTESIAN_POINT ( 'NONE',  ( -0.08000000000000000167, -1.845925619402022155, -0.2644148183989317724 ) ) ;
#35783=EDGE_CURVE ( 'NONE', #30904, #29395, #18651, .T. ) ;
#35787=AXIS2_PLACEMENT_3D ( 'NONE', #30361, #1987, #11228 ) ;
#35798=CARTESIAN_POINT ( 'NONE',  ( -0.05464101615137796630, -1.622350287959229087, -0.08960079202753243321 ) ) ;
#35814=ORIENTED_EDGE ( 'NONE', *, *, #10193, .T. ) ;
#35843=DIRECTION ( 'NONE',  ( 1.000000000000000000, 0.000000000000000000, 0.000000000000000000 ) ) ;
#35850=DIRECTION ( 'NONE',  ( 0.000000000000000000, 0.000000000000000000, -1.000000000000000000 ) ) ;
#35860=ORIENTED_EDGE ( 'NONE', *, *, #17728, .T. ) ;
#35874=DIRECTION ( 'NONE',  ( -1.000000000000000000, -0.000000000000000000, -0.000000000000000000 ) ) ;
#35889=ORIENTED_EDGE ( 'NONE', *, *, #6996, .T. ) ;
#35915=CONICAL_SURFACE ( 'NONE', #21494, 0.01999999999999927530, 1.047197551196600962 ) ;
#35927=ORIENTED_EDGE ( 'NONE', *, *, #39382, .T. ) ;
#35938=EDGE_CURVE ( 'NONE', #20037, #23493, #3008, .T. ) ;
#35962=DIRECTION ( 'NONE',  ( 0.3981087504120402465, 0.9173382270707809427, 0.000000000000000000 ) ) ;
#35981=CARTESIAN_POINT ( 'NONE',  ( -0.02000000000000000042, -2.183180860297908144, -0.4937760292030871079 ) ) ;
#35986=CARTESIAN_POINT ( 'NONE',  ( -0.02000000000000000042, -2.183180860297908144, -0.4937760292030871079 ) ) ;
#35996=DIRECTION ( 'NONE',  ( 0.000000000000000000, 0.8063205929144886541, -0.5914787413272157846 ) ) ;
#36020=FACE_OUTER_BOUND ( 'NONE', #35225, .T. ) ;
#36046=DIRECTION ( 'NONE',  ( 0.000000000000000000, 0.000000000000000000, -1.000000000000000000 ) ) ;
#36061=ORIENTED_EDGE ( 'NONE', *, *, #14426, .F. ) ;
#36064=ORIENTED_EDGE ( 'NONE', *, *, #29485, .T. ) ;
#36085=DIRECTION ( 'NONE',  ( 0.000000000000000000, 0.000000000000000000, -1.000000000000000000 ) ) ;
#36136=CONICAL_SURFACE ( 'NONE', #22361, 0.1400000000000004297, 1.047197551196599630 ) ;
#36142=LINE ( 'NONE', #7954, #21202 ) ;
#36145=EDGE_CURVE ( 'NONE', #5313, #15674, #27241, .T. ) ;
#36162=CONICAL_SURFACE ( 'NONE', #7243, 0.1400000000000012623, 1.047197551196601850 ) ;
#36168=FACE_OUTER_BOUND ( 'NONE', #27568, .T. ) ;
#36184=ADVANCED_FACE ( 'NONE', ( #37098 ), #8913, .F. ) ;
#36189=LINE ( 'NONE', #19961, #20683 ) ;
#36202=ORIENTED_EDGE ( 'NONE', *, *, #26845, .T. ) ;
#36206=CARTESIAN_POINT ( 'NONE',  ( -0.08000000000000000167, -1.712002775963388235, -0.1631032362481502351 ) ) ;
#36239=CARTESIAN_POINT ( 'NONE',  ( -0.02000000000000000042, -1.845925619402022155, -0.2644148183989317724 ) ) ;
#36277=VECTOR ( 'NONE', #6343, 39.37007874015748143 ) ;
#36294=VERTEX_POINT ( 'NONE', #39563 ) ;
#36330=VERTEX_POINT ( 'NONE', #39372 ) ;
#36338=CONICAL_SURFACE ( 'NONE', #29764, 0.4488493849861021068, 1.047197551196599408 ) ;
#36345=CARTESIAN_POINT ( 'NONE',  ( -0.02000000000000000042, -2.551729310907437043, -0.5086726180052709712 ) ) ;
#36349=DIRECTION ( 'NONE',  ( 0.000000000000000000, 0.000000000000000000, -1.000000000000000000 ) ) ;
#36372=AXIS2_PLACEMENT_3D ( 'NONE', #10454, #19921, #1046 ) ;
#36374=CIRCLE ( 'NONE', #14059, 0.1400000000000004297 ) ;
#36389=EDGE_CURVE ( 'NONE', #32357, #16250, #19376, .T. ) ;
#36403=CARTESIAN_POINT ( 'NONE',  ( -0.05464101615137786222, -2.183180860297908144, -0.4937760292030871079 ) ) ;
#36432=AXIS2_PLACEMENT_3D ( 'NONE', #26870, #36528, #7915 ) ;
#36437=DIRECTION ( 'NONE',  ( -1.000000000000000000, -0.000000000000000000, -0.000000000000000000 ) ) ;
#36438=AXIS2_PLACEMENT_3D ( 'NONE', #14377, #14190, #11305 ) ;
#36442=CARTESIAN_POINT ( 'NONE',  ( -0.02000000000000000042, -2.183180860297908144, -0.4937760292030871079 ) ) ;
#36465=VECTOR ( 'NONE', #4226, 39.37007874015748143 ) ;
#36475=CONICAL_SURFACE ( 'NONE', #8218, 0.1400000000000005684, 1.047197551196600962 ) ;
#36481=DIRECTION ( 'NONE',  ( 1.000000000000000000, 0.000000000000000000, 0.000000000000000000 ) ) ;
#36485=EDGE_LOOP ( 'NONE', ( #21064, #7829, #12341, #37745 ) ) ;
#36511=LINE ( 'NONE', #8322, #9410 ) ;
#36525=CARTESIAN_POINT ( 'NONE',  ( -0.02000000000000000042, -2.144840178508589545, -0.3363606153560244616 ) ) ;
#36528=DIRECTION ( 'NONE',  ( -1.000000000000000000, -0.000000000000000000, -0.000000000000000000 ) ) ;
#36531=CARTESIAN_POINT ( 'NONE',  ( -0.02000000000000000042, -2.379949255320110257, -0.6346823614705312533 ) ) ;
#36566=FACE_BOUND ( 'NONE', #28344, .T. ) ;
#36614=CARTESIAN_POINT ( 'NONE',  ( -0.02000000000000000042, -1.598492537578166672, -0.1971380022280825872 ) ) ;
#36621=ORIENTED_EDGE ( 'NONE', *, *, #33838, .T. ) ;
#36637=CARTESIAN_POINT ( 'NONE',  ( -0.05464101615137795936, -1.546789565643408526, -0.06332195561662121164 ) ) ;
#36638=CARTESIAN_POINT ( 'NONE',  ( -0.05464101615137770263, -2.274798198814180772, -0.3601501197397404264 ) ) ;
#36641=CARTESIAN_POINT ( 'NONE',  ( -0.08000000000000000167, -1.772778095317936620, -0.3120197613628934441 ) ) ;
#36642=CARTESIAN_POINT ( 'NONE',  ( -0.02000000000000000042, -2.183180860297908144, -0.4937760292030871079 ) ) ;
#36663=DIRECTION ( 'NONE',  ( 0.000000000000000000, 0.000000000000000000, -1.000000000000000000 ) ) ;
#36676=AXIS2_PLACEMENT_3D ( 'NONE', #38149, #19450, #16552 ) ;
#36718=CARTESIAN_POINT ( 'NONE',  ( -0.02000000000000000042, -2.041899626011815183, -0.6359449730384926225 ) ) ;
#36730=FACE_OUTER_BOUND ( 'NONE', #3135, .T. ) ;
#36753=EDGE_LOOP ( 'NONE', ( #8964, #38189, #37635, #26409, #5401, #33231, #38964, #37129, #36061, #32732, #14556, #16430, #32327, #10731, #14389 ) ) ;
#36827=EDGE_CURVE ( 'NONE', #30658, #5941, #2044, .T. ) ;
#36846=CIRCLE ( 'NONE', #10565, 0.1020173459747799466 ) ;
#36937=CARTESIAN_POINT ( 'NONE',  ( -0.05464101615137787610, -2.183180860297908144, -0.4937760292030871079 ) ) ;
#36938=CARTESIAN_POINT ( 'NONE',  ( -0.05464101615137762630, -1.851224977018630868, -0.7958870385335591324 ) ) ;
#36960=AXIS2_PLACEMENT_3D ( 'NONE', #35798, #39092, #10915 ) ;
#36974=CARTESIAN_POINT ( 'NONE',  ( -0.02000000000000000042, -2.070343076906777213, -0.2454056712452573896 ) ) ;
#36987=AXIS2_PLACEMENT_3D ( 'NONE', #10254, #9829, #439 ) ;
#36993=DIRECTION ( 'NONE',  ( 0.4999999999999979461, 0.7980870686147867321, 0.3362395439413078391 ) ) ;
#37023=ORIENTED_EDGE ( 'NONE', *, *, #36827, .T. ) ;
#37024=AXIS2_PLACEMENT_3D ( 'NONE', #5316, #3081, #21412 ) ;
#37040=LINE ( 'NONE', #6380, #26715 ) ;
#37045=AXIS2_PLACEMENT_3D ( 'NONE', #27224, #19129, #12343 ) ;
#37066=ADVANCED_FACE ( 'NONE', ( #32440 ), #36475, .F. ) ;
#37071=DIRECTION ( 'NONE',  ( 0.4999999999999974465, -0.7980870686147877313, -0.3362395439413060072 ) ) ;
#37091=CARTESIAN_POINT ( 'NONE',  ( -0.08000000000000000167, -2.196538720661423749, -0.6552417777791260667 ) ) ;
#37098=FACE_OUTER_BOUND ( 'NONE', #2249, .T. ) ;
#37103=CARTESIAN_POINT ( 'NONE',  ( -0.05464101615137770263, -1.659335422034822205, 0.2169804935274544377 ) ) ;
#37129=ORIENTED_EDGE ( 'NONE', *, *, #769, .T. ) ;
#37152=PRODUCT_DEFINITION_FORMATION_WITH_SPECIFIED_SOURCE ( 'ANY', '', #13386, .NOT_KNOWN. ) ;
#37161=DIRECTION ( 'NONE',  ( 0.000000000000000000, 0.000000000000000000, -1.000000000000000000 ) ) ;
#37171=PLANE ( 'NONE',  #17529 ) ;
#37173=CYLINDRICAL_SURFACE ( 'NONE', #2210, 0.08000000000000000167 ) ;
#37180=CIRCLE ( 'NONE', #34539, 0.1400000000000013456 ) ;
#37189=CARTESIAN_POINT ( 'NONE',  ( -0.05464101615137796630, -1.750394882718339762, -0.1142373872069606250 ) ) ;
#37196=VERTEX_POINT ( 'NONE', #30175 ) ;
#37337=LINE ( 'NONE', #12639, #10861 ) ;
#37370=DIRECTION ( 'NONE',  ( 1.000000000000000000, 0.000000000000000000, 0.000000000000000000 ) ) ;
#37416=DIRECTION ( 'NONE',  ( 0.000000000000000000, 0.000000000000000000, -1.000000000000000000 ) ) ;
#37461=DIRECTION ( 'NONE',  ( -0.4999999999999962252, -0.8615295495183339369, -0.08812965055383011059 ) ) ;
#37464=ORIENTED_EDGE ( 'NONE', *, *, #23807, .F. ) ;
#37494=CARTESIAN_POINT ( 'NONE',  ( -0.02000000000000000042, -1.845925619402022155, -0.3444148183989317880 ) ) ;
#37554=CARTESIAN_POINT ( 'NONE',  ( -0.02000000000000000042, -1.910390638264138685, -0.8820407338378629669 ) ) ;
#37561=AXIS2_PLACEMENT_3D ( 'NONE', #12116, #15799, #12712 ) ;
#37567=AXIS2_PLACEMENT_3D ( 'NONE', #24761, #15683, #18571 ) ;
#37572=CIRCLE ( 'NONE', #19853, 0.1620173459747806799 ) ;
#37575=DIRECTION ( 'NONE',  ( -1.000000000000000000, -0.000000000000000000, -0.000000000000000000 ) ) ;
#37608=CIRCLE ( 'NONE', #867, 0.08000000000000000167 ) ;
#37613=DIRECTION ( 'NONE',  ( 0.000000000000000000, -0.6595282642760672553, -0.7516797646744243222 ) ) ;
#37635=ORIENTED_EDGE ( 'NONE', *, *, #4666, .T. ) ;
#37664=AXIS2_PLACEMENT_3D ( 'NONE', #14294, #23385, #13868 ) ;
#37692=FACE_OUTER_BOUND ( 'NONE', #11120, .T. ) ;
#37693=ORIENTED_EDGE ( 'NONE', *, *, #19187, .T. ) ;
#37694=EDGE_CURVE ( 'NONE', #1152, #23493, #25125, .T. ) ;
#37728=LINE ( 'NONE', #733, #33112 ) ;
#37740=CARTESIAN_POINT ( 'NONE',  ( -0.02000000000000000042, -2.183180860297908144, -0.4937760292030871079 ) ) ;
#37745=ORIENTED_EDGE ( 'NONE', *, *, #36145, .F. ) ;
#37760=CIRCLE ( 'NONE', #8177, 0.07999999999999996003 ) ;
#37787=DIRECTION ( 'NONE',  ( 1.000000000000000000, 0.000000000000000000, 0.000000000000000000 ) ) ;
#37796=AXIS2_PLACEMENT_3D ( 'NONE', #3910, #23267, #39086 ) ;
#37816=VERTEX_POINT ( 'NONE', #19752 ) ;
#37833=AXIS2_PLACEMENT_3D ( 'NONE', #38622, #22615, #28954 ) ;
#37854=ORIENTED_EDGE ( 'NONE', *, *, #3120, .T. ) ;
#37858=FACE_OUTER_BOUND ( 'NONE', #19729, .T. ) ;
#37862=ORIENTED_EDGE ( 'NONE', *, *, #38123, .F. ) ;
#37865=AXIS2_PLACEMENT_3D ( 'NONE', #1562, #30134, #26853 ) ;
#37868=ADVANCED_FACE ( 'NONE', ( #32101 ), #4284, .F. ) ;
#37892=ORIENTED_EDGE ( 'NONE', *, *, #14278, .T. ) ;
#37905=VERTEX_POINT ( 'NONE', #23055 ) ;
#37941=ORIENTED_EDGE ( 'NONE', *, *, #387, .T. ) ;
#37942=FACE_OUTER_BOUND ( 'NONE', #19718, .T. ) ;
#37944=DIRECTION ( 'NONE',  ( 0.000000000000000000, 0.000000000000000000, -1.000000000000000000 ) ) ;
#37958=CARTESIAN_POINT ( 'NONE',  ( -0.08000000000000000167, -2.023118915020511999, -0.4686803309516410221 ) ) ;
#37968=CARTESIAN_POINT ( 'NONE',  ( -0.02000000000000000042, -1.598492537578166672, -0.1971380022280825872 ) ) ;
#37978=DIRECTION ( 'NONE',  ( 1.000000000000000000, -0.000000000000000000, -0.000000000000000000 ) ) ;
#37987=VERTEX_POINT ( 'NONE', #11518 ) ;
#37994=LINE ( 'NONE', #412, #24706 ) ;
#37996=ORIENTED_EDGE ( 'NONE', *, *, #13768, .F. ) ;
#38006=VERTEX_POINT ( 'NONE', #17870 ) ;
#38011=ORIENTED_EDGE ( 'NONE', *, *, #35182, .T. ) ;
#38016=ORIENTED_EDGE ( 'NONE', *, *, #30034, .F. ) ;
#38035=ORIENTED_EDGE ( 'NONE', *, *, #3230, .F. ) ;
#38039=DIRECTION ( 'NONE',  ( 0.000000000000000000, 0.000000000000000000, -1.000000000000000000 ) ) ;
#38044=ORIENTED_EDGE ( 'NONE', *, *, #15699, .T. ) ;
#38048=DIRECTION ( 'NONE',  ( 0.000000000000000000, -0.6595282642760673664, -0.7516797646744242112 ) ) ;
#38103=AXIS2_PLACEMENT_3D ( 'NONE', #11897, #11505, #21782 ) ;
#38107=AXIS2_PLACEMENT_3D ( 'NONE', #28967, #16634, #34946 ) ;
#38123=EDGE_CURVE ( 'NONE', #22522, #19084, #34507, .T. ) ;
#38149=CARTESIAN_POINT ( 'NONE',  ( -0.08000000000000000167, -2.626773565144302935, -0.2726934094652516127 ) ) ;
#38189=ORIENTED_EDGE ( 'NONE', *, *, #13768, .T. ) ;
#38191=CIRCLE ( 'NONE', #9940, 0.01999999999999927530 ) ;
#38193=ORIENTED_EDGE ( 'NONE', *, *, #14239, .F. ) ;
#38200=VECTOR ( 'NONE', #22415, 39.37007874015748143 ) ;
#38215=CARTESIAN_POINT ( 'NONE',  ( -0.02000000000000000042, -1.614234636154356251, 0.1774087976708900172 ) ) ;
#38246=VECTOR ( 'NONE', #15135, 39.37007874015748143 ) ;
#38248=ORIENTED_EDGE ( 'NONE', *, *, #1498, .F. ) ;
#38288=ORIENTED_EDGE ( 'NONE', *, *, #21313, .F. ) ;
#38308=VECTOR ( 'NONE', #30187, 39.37007874015748143 ) ;
#38313=DIMENSIONAL_EXPONENTS ( 1.000000000000000000, 0.000000000000000000, 0.000000000000000000, 0.000000000000000000, 0.000000000000000000, 0.000000000000000000, 0.000000000000000000 ) ;
#38320=LINE ( 'NONE', #16522, #38526 ) ;
#38333=ORIENTED_EDGE ( 'NONE', *, *, #17301, .T. ) ;
#38336=CONICAL_SURFACE ( 'NONE', #12070, 0.1400000000000007627, 1.047197551196601406 ) ;
#38360=EDGE_CURVE ( 'NONE', #20037, #7253, #10041, .T. ) ;
#38364=CARTESIAN_POINT ( 'NONE',  ( -0.02000000000000000042, -1.910390638264138685, -0.7420407338378623985 ) ) ;
#38381=CARTESIAN_POINT ( 'NONE',  ( -0.02000000000000000042, -2.071870001606465284, -0.3441689154348898105 ) ) ;
#38413=EDGE_CURVE ( 'NONE', #38795, #34243, #20127, .T. ) ;
#38433=EDGE_CURVE ( 'NONE', #25698, #10115, #22760, .T. ) ;
#38437=CARTESIAN_POINT ( 'NONE',  ( -0.05464101615137770263, -2.589364949149576933, -0.2950346662398796171 ) ) ;
#38445=ORIENTED_EDGE ( 'NONE', *, *, #19710, .T. ) ;
#38460=DIRECTION ( 'NONE',  ( -0.4999999999999974465, 0.7980870686147877313, 0.3362395439413060072 ) ) ;
#38473=DIRECTION ( 'NONE',  ( 0.000000000000000000, 0.000000000000000000, -1.000000000000000000 ) ) ;
#38486=CARTESIAN_POINT ( 'NONE',  ( -0.02000000000000000042, -1.682484669133182953, -0.03683853088544706417 ) ) ;
#38501=ORIENTED_EDGE ( 'NONE', *, *, #1886, .T. ) ;
#38526=VECTOR ( 'NONE', #40328, 39.37007874015748143 ) ;
#38545=EDGE_CURVE ( 'NONE', #17659, #15479, #37180, .T. ) ;
#38566=EDGE_CURVE ( 'NONE', #25808, #5617, #14751, .T. ) ;
#38568=DIRECTION ( 'NONE',  ( 1.000000000000000000, -0.000000000000000000, -0.000000000000000000 ) ) ;
#38581=EDGE_LOOP ( 'NONE', ( #5293, #33221, #35889, #38193 ) ) ;
#38622=CARTESIAN_POINT ( 'NONE',  ( -0.08000000000000000167, -2.551729310907437043, -0.5086726180052709712 ) ) ;
#38623=CARTESIAN_POINT ( 'NONE',  ( -0.05464101615137795243, -1.669835911085076674, -0.2333336242928227000 ) ) ;
#38631=DIRECTION ( 'NONE',  ( 1.000000000000000000, 0.000000000000000000, 0.000000000000000000 ) ) ;
#38636=EDGE_LOOP ( 'NONE', ( #1332, #14260, #265, #31457 ) ) ;
#38640=EDGE_LOOP ( 'NONE', ( #18103, #24897, #40535, #12381 ) ) ;
#38642=DIRECTION ( 'NONE',  ( 0.000000000000000000, 0.000000000000000000, -1.000000000000000000 ) ) ;
#38667=EDGE_CURVE ( 'NONE', #10794, #33645, #3038, .T. ) ;
#38672=ADVANCED_FACE ( 'NONE', ( #28509 ), #34874, .F. ) ;
#38678=ORIENTED_EDGE ( 'NONE', *, *, #12169, .F. ) ;
#38686=CARTESIAN_POINT ( 'NONE',  ( -0.02000000000000000042, -1.968175500587574067, -0.6048844944454191408 ) ) ;
#38688=DIRECTION ( 'NONE',  ( 1.000000000000000000, -0.000000000000000000, -0.000000000000000000 ) ) ;
#38716=DIRECTION ( 'NONE',  ( -1.000000000000000000, -0.000000000000000000, -0.000000000000000000 ) ) ;
#38736=DIRECTION ( 'NONE',  ( -1.000000000000000000, 0.000000000000000000, 0.000000000000000000 ) ) ;
#38740=DIRECTION ( 'NONE',  ( 1.000000000000000000, 0.000000000000000000, 0.000000000000000000 ) ) ;
#38741=EDGE_LOOP ( 'NONE', ( #30855, #4293, #30189, #26355 ) ) ;
#38774=ORIENTED_EDGE ( 'NONE', *, *, #20755, .F. ) ;
#38792=VERTEX_POINT ( 'NONE', #29518 ) ;
#38795=VERTEX_POINT ( 'NONE', #32999 ) ;
#38802=EDGE_CURVE ( 'NONE', #18990, #12086, #14293, .T. ) ;
#38808=FACE_OUTER_BOUND ( 'NONE', #26930, .T. ) ;
#38826=DIRECTION ( 'NONE',  ( -0.4999999999999971134, -0.5122356157878134031, -0.6982941170584801016 ) ) ;
#38834=VECTOR ( 'NONE', #37071, 39.37007874015748854 ) ;
#38842=ORIENTED_EDGE ( 'NONE', *, *, #31693, .F. ) ;
#38872=PRODUCT_DEFINITION_CONTEXT ( 'detailed design', #29256, 'design' ) ;
#38880=EDGE_CURVE ( 'NONE', #40536, #12086, #16196, .T. ) ;
#38894=CIRCLE ( 'NONE', #17867, 0.1020173459747797384 ) ;
#38919=( LENGTH_UNIT ( ) NAMED_UNIT ( * ) SI_UNIT ( $, .METRE. ) );
#38964=ORIENTED_EDGE ( 'NONE', *, *, #1226, .T. ) ;
#38967=DIRECTION ( 'NONE',  ( 1.000000000000000000, 0.000000000000000000, 0.000000000000000000 ) ) ;
#38973=DIRECTION ( 'NONE',  ( -1.000000000000000000, 0.000000000000000000, 0.000000000000000000 ) ) ;
#39016=DIRECTION ( 'NONE',  ( 0.000000000000000000, 0.000000000000000000, -1.000000000000000000 ) ) ;
#39039=DIRECTION ( 'NONE',  ( -0.4999999999999972800, 0.000000000000000000, 0.8660254037844402619 ) ) ;
#39040=DIRECTION ( 'NONE',  ( 0.000000000000000000, -1.328828465659078041E-14, -1.000000000000000000 ) ) ;
#39062=ADVANCED_FACE ( 'NONE', ( #8929 ), #39851, .T. ) ;
#39073=DIRECTION ( 'NONE',  ( 0.000000000000000000, 0.000000000000000000, -1.000000000000000000 ) ) ;
#39075=FACE_OUTER_BOUND ( 'NONE', #38581, .T. ) ;
#39086=DIRECTION ( 'NONE',  ( 0.000000000000000000, 0.000000000000000000, -1.000000000000000000 ) ) ;
#39092=DIRECTION ( 'NONE',  ( 1.000000000000000000, -0.000000000000000000, -0.000000000000000000 ) ) ;
#39143=CIRCLE ( 'NONE', #5621, 0.08000000000000000167 ) ;
#39158=ORIENTED_EDGE ( 'NONE', *, *, #6617, .F. ) ;
#39189=CARTESIAN_POINT ( 'NONE',  ( -0.08000000000000000167, -1.599201040860868339, 0.1642182323853691728 ) ) ;
#39221=CARTESIAN_POINT ( 'NONE',  ( -0.02000000000000000042, -2.626773565144302935, -0.2726934094652516127 ) ) ;
#39239=DIRECTION ( 'NONE',  ( 0.4999999999999974465, -0.4440468346413919409, -0.7435202812600089084 ) ) ;
#39244=DIRECTION ( 'NONE',  ( 1.000000000000000000, 0.000000000000000000, 0.000000000000000000 ) ) ;
#39249=CARTESIAN_POINT ( 'NONE',  ( -0.02000000000000000042, -2.022243545323729741, -0.2876084842891860061 ) ) ;
#39277=CARTESIAN_POINT ( 'NONE',  ( -0.02000000000000000042, -2.332630956013932888, -0.5701767140373721343 ) ) ;
#39280=CARTESIAN_POINT ( 'NONE',  ( -0.08000000000000000167, -1.845925619402022155, -0.3444148183989317880 ) ) ;
#39314=LINE ( 'NONE', #36638, #15238 ) ;
#39318=CYLINDRICAL_SURFACE ( 'NONE', #12239, 0.1620173459747806799 ) ;
#39332=CARTESIAN_POINT ( 'NONE',  ( -0.08000000000000000167, -2.070343076906777213, -0.2454056712452573896 ) ) ;
#39339=EDGE_CURVE ( 'NONE', #36294, #26509, #38320, .T. ) ;
#39341=CARTESIAN_POINT ( 'NONE',  ( -0.02000000000000000042, -2.551729310907437043, -0.5086726180052709712 ) ) ;
#39344=VERTEX_POINT ( 'NONE', #15648 ) ;
#39370=ORIENTED_EDGE ( 'NONE', *, *, #6439, .T. ) ;
#39372=CARTESIAN_POINT ( 'NONE',  ( -0.02000000000000000042, -1.459219328725982034, -0.1828911325362468643 ) ) ;
#39382=EDGE_CURVE ( 'NONE', #36294, #12543, #37040, .T. ) ;
#39383=DIRECTION ( 'NONE',  ( 0.4999999999999962252, -0.6509737717187612516, 0.5711682313769330666 ) ) ;
#39386=LINE ( 'NONE', #34429, #24129 ) ;
#39397=ADVANCED_FACE ( 'NONE', ( #21441 ), #35915, .T. ) ;
#39409=VERTEX_POINT ( 'NONE', #15234 ) ;
#39429=CARTESIAN_POINT ( 'NONE',  ( -0.02000000000000000042, -1.598492537578166672, -0.1971380022280825872 ) ) ;
#39430=FACE_OUTER_BOUND ( 'NONE', #30025, .T. ) ;
#39440=CARTESIAN_POINT ( 'NONE',  ( -0.02000000000000000042, -2.551729310907437043, -0.4286726180052709001 ) ) ;
#39457=AXIS2_PLACEMENT_3D ( 'NONE', #34550, #15021, #40095 ) ;
#39466=CARTESIAN_POINT ( 'NONE',  ( -0.02000000000000000042, -2.626773565144302935, -0.2726934094652516127 ) ) ;
#39484=CIRCLE ( 'NONE', #21775, 0.1400000000000007350 ) ;
#39503=AXIS2_PLACEMENT_3D ( 'NONE', #14930, #40211, #5661 ) ;
#39507=CARTESIAN_POINT ( 'NONE',  ( -0.02000000000000000042, -2.183180860297908144, -0.4937760292030871079 ) ) ;
#39528=AXIS2_PLACEMENT_3D ( 'NONE', #22446, #16271, #38473 ) ;
#39529=LINE ( 'NONE', #32959, #8976 ) ;
#39539=CARTESIAN_POINT ( 'NONE',  ( -0.08000000000000000167, -2.585754275622221154, -0.2040099479399058724 ) ) ;
#39541=EDGE_LOOP ( 'NONE', ( #30524, #24546, #121, #21912 ) ) ;
#39544=ORIENTED_EDGE ( 'NONE', *, *, #5982, .F. ) ;
#39563=CARTESIAN_POINT ( 'NONE',  ( -0.05464101615137766793, -2.548345659627495596, -0.2263512047145338768 ) ) ;
#39585=EDGE_LOOP ( 'NONE', ( #17848, #14256, #9747, #18062 ) ) ;
#39587=CONICAL_SURFACE ( 'NONE', #17259, 0.1400000000000009570, 1.047197551196600518 ) ;
#39589=EDGE_CURVE ( 'NONE', #4481, #16266, #35129, .T. ) ;
#39595=LINE ( 'NONE', #36718, #40122 ) ;
#39623=CARTESIAN_POINT ( 'NONE',  ( -0.05464101615137787610, -2.504411011601259673, -0.4441669705721119632 ) ) ;
#39629=AXIS2_PLACEMENT_3D ( 'NONE', #5693, #39852, #2422 ) ;
#39644=LINE ( 'NONE', #26910, #16012 ) ;
#39654=ORIENTED_EDGE ( 'NONE', *, *, #19758, .T. ) ;
#39691=EDGE_CURVE ( 'NONE', #7866, #14928, #35726, .T. ) ;
#39701=CARTESIAN_POINT ( 'NONE',  ( -0.05464101615137785528, -2.198867511061768809, -0.9423512173156428640 ) ) ;
#39727=DIRECTION ( 'NONE',  ( 0.000000000000000000, 0.000000000000000000, -1.000000000000000000 ) ) ;
#39735=CARTESIAN_POINT ( 'NONE',  ( -0.02000000000000000042, -2.183180860297908144, -0.4937760292030871079 ) ) ;
#39748=DIRECTION ( 'NONE',  ( 1.000000000000000000, -0.000000000000000000, -0.000000000000000000 ) ) ;
#39767=CARTESIAN_POINT ( 'NONE',  ( -0.05464101615137762630, -2.004218822785767795, -0.4035264592197354561 ) ) ;
#39771=CYLINDRICAL_SURFACE ( 'NONE', #13331, 0.1620173459747806799 ) ;
#39779=ORIENTED_EDGE ( 'NONE', *, *, #2725, .F. ) ;
#39788=VECTOR ( 'NONE', #39239, 39.37007874015748854 ) ;
#39795=EDGE_CURVE ( 'NONE', #35302, #28686, #7317, .T. ) ;
#39811=CARTESIAN_POINT ( 'NONE',  ( -0.02000000000000000042, -1.765869171405739957, -0.8132390237819782097 ) ) ;
#39850=FACE_BOUND ( 'NONE', #23085, .T. ) ;
#39851=CONICAL_SURFACE ( 'NONE', #3070, 0.5756329413417603513, 1.047197551196602738 ) ;
#39852=DIRECTION ( 'NONE',  ( 1.000000000000000000, 0.000000000000000000, 0.000000000000000000 ) ) ;
#39858=CARTESIAN_POINT ( 'NONE',  ( -0.02000000000000000042, -2.644673614468930012, -0.2637721856604205439 ) ) ;
#39870=ORIENTED_EDGE ( 'NONE', *, *, #30240, .T. ) ;
#39886=CARTESIAN_POINT ( 'NONE',  ( -0.02000000000000000042, -2.626773565144302935, -0.2726934094652516127 ) ) ;
#39894=CARTESIAN_POINT ( 'NONE',  ( -0.08000000000000000167, -1.944084441611813707, -0.4562887203618206655 ) ) ;
#39915=EDGE_LOOP ( 'NONE', ( #8485, #27216, #24095, #39544 ) ) ;
#39916=ORIENTED_EDGE ( 'NONE', *, *, #15477, .T. ) ;
#39921=CARTESIAN_POINT ( 'NONE',  ( -0.02000000000000000042, -1.599201040860868339, 0.1642182323853691728 ) ) ;
#39927=ORIENTED_EDGE ( 'NONE', *, *, #26242, .F. ) ;
#39942=CARTESIAN_POINT ( 'NONE',  ( -0.02000000000000000042, -1.968175500587574067, -0.6048844944454191408 ) ) ;
#39953=CARTESIAN_POINT ( 'NONE',  ( -0.08000000000000000167, -2.314906514113384883, -0.5881050943081593818 ) ) ;
#39978=DIRECTION ( 'NONE',  ( 1.000000000000000000, 0.000000000000000000, 0.000000000000000000 ) ) ;
#40009=ORIENTED_EDGE ( 'NONE', *, *, #15699, .F. ) ;
#40048=FACE_OUTER_BOUND ( 'NONE', #38741, .T. ) ;
#40062=VECTOR ( 'NONE', #36993, 39.37007874015748854 ) ;
#40095=DIRECTION ( 'NONE',  ( 0.000000000000000000, 0.000000000000000000, 1.000000000000000000 ) ) ;
#40104=EDGE_LOOP ( 'NONE', ( #27659, #11083, #8035, #16991 ) ) ;
#40122=VECTOR ( 'NONE', #30345, 39.37007874015748143 ) ;
#40125=EDGE_CURVE ( 'NONE', #15479, #10881, #10437, .T. ) ;
#40134=DIRECTION ( 'NONE',  ( -1.000000000000000000, -0.000000000000000000, -0.000000000000000000 ) ) ;
#40171=ADVANCED_FACE ( 'NONE', ( #9826 ), #32349, .T. ) ;
#40196=EDGE_LOOP ( 'NONE', ( #4531, #24674, #9628, #26413 ) ) ;
#40211=DIRECTION ( 'NONE',  ( -0.8660254037844401509, 0.2957393706636063380, 0.4031602964572422731 ) ) ;
#40241=DIRECTION ( 'NONE',  ( 0.000000000000000000, 0.000000000000000000, -1.000000000000000000 ) ) ;
#40250=CARTESIAN_POINT ( 'NONE',  ( -0.05464101615137796630, -1.682484669133182953, -0.03683853088544706417 ) ) ;
#40281=CIRCLE ( 'NONE', #14673, 0.07999999999999996003 ) ;
#40287=DIRECTION ( 'NONE',  ( 0.000000000000000000, 0.6595282642760668113, 0.7516797646744246553 ) ) ;
#40311=EDGE_CURVE ( 'NONE', #7871, #21046, #27117, .T. ) ;
#40323=CARTESIAN_POINT ( 'NONE',  ( -0.05464101615137761936, -2.041899626011815183, -0.6359449730384926225 ) ) ;
#40324=CARTESIAN_POINT ( 'NONE',  ( -0.05464101615137796630, -1.622350287959229087, -0.009600792027532436754 ) ) ;
#40328=DIRECTION ( 'NONE',  ( -1.000000000000000000, 0.000000000000000000, 0.000000000000000000 ) ) ;
#40335=CIRCLE ( 'NONE', #27219, 0.1020173459747800854 ) ;
#40337=CIRCLE ( 'NONE', #25918, 0.08000000000000002942 ) ;
#40353=ADVANCED_FACE ( 'NONE', ( #30979 ), #2803, .T. ) ;
#40359=CONICAL_SURFACE ( 'NONE', #10801, 0.1400000000000007350, 1.047197551196601184 ) ;
#40365=EDGE_CURVE ( 'NONE', #38006, #26267, #14623, .T. ) ;
#40371=AXIS2_PLACEMENT_3D ( 'NONE', #36974, #5706, #31230 ) ;
#40393=VECTOR ( 'NONE', #11936, 39.37007874015748854 ) ;
#40426=EDGE_LOOP ( 'NONE', ( #11646, #32643, #10567, #25556 ) ) ;
#40448=CARTESIAN_POINT ( 'NONE',  ( -0.02000000000000000042, -2.032088213807425880, -0.4352898549974345555 ) ) ;
#40458=FACE_OUTER_BOUND ( 'NONE', #23194, .T. ) ;
#40470=ORIENTED_EDGE ( 'NONE', *, *, #20282, .T. ) ;
#40479=ORIENTED_EDGE ( 'NONE', *, *, #6421, .F. ) ;
#40528=CARTESIAN_POINT ( 'NONE',  ( -0.02000000000000000042, -1.599201040860868339, 0.1642182323853691728 ) ) ;
#40535=ORIENTED_EDGE ( 'NONE', *, *, #27885, .T. ) ;
#40536=VERTEX_POINT ( 'NONE', #29107 ) ;
#40587=DIRECTION ( 'NONE',  ( -1.000000000000000000, -0.000000000000000000, -0.000000000000000000 ) ) ;
#40588=ADVANCED_FACE ( 'NONE', ( #25625 ), #10724, .F. ) ;
#40596=DIRECTION ( 'NONE',  ( 0.000000000000000000, -7.757484229545264892E-16, -1.000000000000000000 ) ) ;
#40603=AXIS2_PLACEMENT_3D ( 'NONE', #36937, #28283, #9572 ) ;
#40614=VERTEX_POINT ( 'NONE', #1351 ) ;
#40616=CARTESIAN_POINT ( 'NONE',  ( -0.02000000000000000042, -2.379949255320110257, -0.6346823614705312533 ) ) ;
#40630=CARTESIAN_POINT ( 'NONE',  ( -0.02000000000000000042, -2.314906514113384883, -0.5881050943081593818 ) ) ;
#40681=COLOUR_RGB('Sky Blue',0.24,0.69,0.87);
#40682=FILL_AREA_STYLE_COLOUR('',#40681);
#40683=FILL_AREA_STYLE('',(#40682));
#40684=SURFACE_STYLE_FILL_AREA(#40683);
#40685=SURFACE_SIDE_STYLE('',(#40684));
#40686=SURFACE_STYLE_USAGE(.BOTH.,#40685);
#40687=PRESENTATION_STYLE_ASSIGNMENT((#40686));
#40710=STYLED_ITEM('',(#40687),#19265);
#40721=MECHANICAL_DESIGN_GEOMETRIC_PRESENTATION_REPRESENTATION('',(#40710),#11399);
ENDSEC;
END-ISO-10303-21;
